ISO-10303-21;
HEADER;
/* Generated by software containing ST-Developer
 * from STEP Tools, Inc. (www.steptools.com) 
 */

FILE_DESCRIPTION(
/* description */ ('Pipe clamp stand with threaded column'),
/* implementation_level */ '2;1');

FILE_NAME(
/* name */ 'M24 adjustment nut.step',
/* time_stamp */ '2026-10-27T10:55:48-07:00',
/* author */ (''),
/* organization */ (''),
/* preprocessor_version */ 'ST-DEVELOPER v20.2',
/* originating_system */ 'Autodesk Translation Framework v15.17.0.0',
/* authorisation */ '');

FILE_SCHEMA (('AUTOMOTIVE_DESIGN { 1 0 10303 214 3 1 1 }'));
ENDSEC;

DATA;
#10=MECHANICAL_DESIGN_GEOMETRIC_PRESENTATION_REPRESENTATION('',(#767),#34433);
#209=B_SPLINE_SURFACE_WITH_KNOTS('',3,3,((#29392,#29393,#29394,#29395,#29396,
#29397,#29398,#29399,#29400,#29401,#29402,#29403,#29404,#29405,#29406,#29407,
#29408,#29409,#29410,#29411,#29412,#29413,#29414,#29415,#29416,#29417,#29418,
#29419,#29420,#29421,#29422,#29423,#29424,#29425,#29426,#29427,#29428,#29429,
#29430,#29431,#29432,#29433,#29434,#29435,#29436,#29437,#29438,#29439,#29440,
#29441,#29442,#29443,#29444,#29445,#29446,#29447,#29448,#29449,#29450),
(#29451,#29452,#29453,#29454,#29455,#29456,#29457,#29458,#29459,#29460,
#29461,#29462,#29463,#29464,#29465,#29466,#29467,#29468,#29469,#29470,#29471,
#29472,#29473,#29474,#29475,#29476,#29477,#29478,#29479,#29480,#29481,#29482,
#29483,#29484,#29485,#29486,#29487,#29488,#29489,#29490,#29491,#29492,#29493,
#29494,#29495,#29496,#29497,#29498,#29499,#29500,#29501,#29502,#29503,#29504,
#29505,#29506,#29507,#29508,#29509),(#29510,#29511,#29512,#29513,#29514,
#29515,#29516,#29517,#29518,#29519,#29520,#29521,#29522,#29523,#29524,#29525,
#29526,#29527,#29528,#29529,#29530,#29531,#29532,#29533,#29534,#29535,#29536,
#29537,#29538,#29539,#29540,#29541,#29542,#29543,#29544,#29545,#29546,#29547,
#29548,#29549,#29550,#29551,#29552,#29553,#29554,#29555,#29556,#29557,#29558,
#29559,#29560,#29561,#29562,#29563,#29564,#29565,#29566,#29567,#29568),
(#29569,#29570,#29571,#29572,#29573,#29574,#29575,#29576,#29577,#29578,
#29579,#29580,#29581,#29582,#29583,#29584,#29585,#29586,#29587,#29588,#29589,
#29590,#29591,#29592,#29593,#29594,#29595,#29596,#29597,#29598,#29599,#29600,
#29601,#29602,#29603,#29604,#29605,#29606,#29607,#29608,#29609,#29610,#29611,
#29612,#29613,#29614,#29615,#29616,#29617,#29618,#29619,#29620,#29621,#29622,
#29623,#29624,#29625,#29626,#29627)),.UNSPECIFIED.,.F.,.F.,.F.,(4,4),(4,
1,1,1,1,1,1,1,1,1,1,1,1,1,1,1,1,1,1,1,1,1,1,1,1,1,1,1,1,1,1,1,1,1,1,1,1,
1,1,1,1,1,1,1,1,1,1,1,1,1,1,1,1,1,1,1,4),(0.,0.193239135097769),(11.8520359647449,
12.3369705490202,12.8219051332955,13.3068397175708,13.7917743018461,14.2767088861213,
14.7616434703966,15.2465780546719,15.7315126389472,16.2164472232225,16.7013818074977,
17.186316391773,17.6712509760483,18.1561855603236,18.6411201445989,19.1260547288741,
19.6109893131494,20.0959238974247,20.5808584817,21.0657930659752,21.5507276502505,
22.0356622345258,22.5205968188011,23.0055314030764,23.4904659873516,23.9754005716269,
24.4603351559022,24.9452697401775,25.4302043244528,25.915138908728,26.4000734930033,
26.8850080772786,27.3699426615539,27.8548772458292,28.3398118301044,28.8247464143797,
29.309680998655,29.7946155829303,30.2795501672055,30.7644847514808,31.2494193357561,
31.7343539200314,32.2192885043067,32.7042230885819,33.1891576728572,33.6740922571325,
34.1590268414078,34.6439614256831,35.1288960099583,35.6138305942336,36.0987651785089,
36.5836997627842,37.0686343470595,37.5535689313347,38.03850351561,38.5234380998853,
39.0083726841606),.UNSPECIFIED.);
#210=B_SPLINE_SURFACE_WITH_KNOTS('',3,3,((#29826,#29827,#29828,#29829,#29830,
#29831,#29832,#29833,#29834,#29835,#29836,#29837,#29838,#29839,#29840,#29841,
#29842,#29843,#29844,#29845,#29846,#29847,#29848,#29849,#29850,#29851,#29852,
#29853,#29854,#29855,#29856,#29857,#29858,#29859,#29860,#29861,#29862,#29863,
#29864,#29865,#29866,#29867,#29868,#29869,#29870,#29871,#29872,#29873,#29874,
#29875,#29876,#29877,#29878,#29879,#29880,#29881,#29882,#29883,#29884),
(#29885,#29886,#29887,#29888,#29889,#29890,#29891,#29892,#29893,#29894,
#29895,#29896,#29897,#29898,#29899,#29900,#29901,#29902,#29903,#29904,#29905,
#29906,#29907,#29908,#29909,#29910,#29911,#29912,#29913,#29914,#29915,#29916,
#29917,#29918,#29919,#29920,#29921,#29922,#29923,#29924,#29925,#29926,#29927,
#29928,#29929,#29930,#29931,#29932,#29933,#29934,#29935,#29936,#29937,#29938,
#29939,#29940,#29941,#29942,#29943),(#29944,#29945,#29946,#29947,#29948,
#29949,#29950,#29951,#29952,#29953,#29954,#29955,#29956,#29957,#29958,#29959,
#29960,#29961,#29962,#29963,#29964,#29965,#29966,#29967,#29968,#29969,#29970,
#29971,#29972,#29973,#29974,#29975,#29976,#29977,#29978,#29979,#29980,#29981,
#29982,#29983,#29984,#29985,#29986,#29987,#29988,#29989,#29990,#29991,#29992,
#29993,#29994,#29995,#29996,#29997,#29998,#29999,#30000,#30001,#30002),
(#30003,#30004,#30005,#30006,#30007,#30008,#30009,#30010,#30011,#30012,
#30013,#30014,#30015,#30016,#30017,#30018,#30019,#30020,#30021,#30022,#30023,
#30024,#30025,#30026,#30027,#30028,#30029,#30030,#30031,#30032,#30033,#30034,
#30035,#30036,#30037,#30038,#30039,#30040,#30041,#30042,#30043,#30044,#30045,
#30046,#30047,#30048,#30049,#30050,#30051,#30052,#30053,#30054,#30055,#30056,
#30057,#30058,#30059,#30060,#30061)),.UNSPECIFIED.,.F.,.F.,.F.,(4,4),(4,
1,1,1,1,1,1,1,1,1,1,1,1,1,1,1,1,1,1,1,1,1,1,1,1,1,1,1,1,1,1,1,1,1,1,1,1,
1,1,1,1,1,1,1,1,1,1,1,1,1,1,1,1,1,1,1,4),(0.,0.193239135097769),(14.3987024268659,
14.8836370111412,15.3685715954165,15.8535061796917,16.338440763967,16.8233753482423,
17.3083099325176,17.7932445167929,18.2781791010681,18.7631136853434,19.2480482696187,
19.732982853894,20.2179174381693,20.7028520224445,21.1877866067198,21.6727211909951,
22.1576557752704,22.6425903595457,23.1275249438209,23.6124595280962,24.0973941123715,
24.5823286966468,25.067263280922,25.5521978651973,26.0371324494726,26.5220670337479,
27.0070016180232,27.4919362022984,27.9768707865737,28.461805370849,28.9467399551243,
29.4316745393996,29.9166091236748,30.4015437079501,30.8864782922254,31.3714128765007,
31.856347460776,32.3412820450512,32.8262166293265,33.3111512136018,33.7960857978771,
34.2810203821523,34.7659549664276,35.2508895507029,35.7358241349782,36.2207587192535,
36.7056933035287,37.190627887804,37.6755624720793,38.1604970563546,38.6454316406299,
39.1303662249051,39.6153008091804,40.1002353934557,40.585169977731,41.0701045620063,
41.5550391462815),.UNSPECIFIED.);
#601=B_SPLINE_CURVE_WITH_KNOTS('',3,(#28950,#28951,#28952,#28953,#28954,
#28955,#28956),.UNSPECIFIED.,.F.,.F.,(4,3,4),(26.4420020698014,26.6714021351404,
27.1563367194156),.UNSPECIFIED.);
#602=B_SPLINE_CURVE_WITH_KNOTS('',3,(#28959,#28960,#28961,#28962,#28963,
#28964,#28965,#28966,#28967,#28968,#28969,#28970,#28971,#28972,#28973,#28974,
#28975,#28976,#28977),.UNSPECIFIED.,.F.,.F.,(4,3,3,3,3,3,4),(-25.1327412287183,
-24.7316637980392,-24.2467292137639,-23.7617946294887,-23.2768600452134,
-22.7919254609381,-22.7054832247428),.UNSPECIFIED.);
#603=B_SPLINE_CURVE_WITH_KNOTS('',3,(#28982,#28983,#28984,#28985,#28986,
#28987,#28988,#28989,#28990,#28991,#28992,#28993,#28994,#28995,#28996,#28997,
#28998,#28999,#29000,#29001,#29002,#29003,#29004,#29005,#29006,#29007,#29008,
#29009,#29010,#29011,#29012,#29013,#29014,#29015,#29016,#29017,#29018,#29019,
#29020,#29021,#29022,#29023,#29024),.UNSPECIFIED.,.F.,.F.,(4,3,3,3,3,3,
3,3,3,3,3,3,3,3,4),(20.1588167626218,20.3672525395617,20.852187123837,21.3371217081123,
21.8220562923876,22.3069908766628,22.7919254609381,23.2768600452134,23.7617946294887,
24.246729213764,24.7316637980392,25.2165983823145,25.7015329665898,26.1864675508651,
26.4420020698014),.UNSPECIFIED.);
#604=B_SPLINE_CURVE_WITH_KNOTS('',3,(#29025,#29026,#29027,#29028,#29029,
#29030,#29031,#29032,#29033,#29034,#29035,#29036,#29037,#29038,#29039,#29040,
#29041,#29042,#29043,#29044,#29045,#29046,#29047,#29048,#29049,#29050,#29051,
#29052,#29053,#29054,#29055,#29056,#29057,#29058,#29059,#29060,#29061,#29062,
#29063,#29064,#29065,#29066,#29067),.UNSPECIFIED.,.F.,.F.,(4,3,3,3,3,3,
3,3,3,3,3,3,3,3,4),(-22.7054832247428,-22.3069908766628,-21.8220562923876,
-21.3371217081123,-20.852187123837,-20.3672525395617,-19.8823179552864,
-19.3973833710112,-18.9124487867359,-18.4275142024606,-17.9425796181853,
-17.45764503391,-16.9727104496348,-16.4877758653595,-16.4222979175632),
 .UNSPECIFIED.);
#605=B_SPLINE_CURVE_WITH_KNOTS('',3,(#29072,#29073,#29074,#29075,#29076,
#29077,#29078,#29079,#29080,#29081,#29082,#29083,#29084,#29085,#29086,#29087,
#29088,#29089,#29090,#29091,#29092,#29093,#29094,#29095,#29096,#29097,#29098,
#29099,#29100,#29101,#29102,#29103,#29104,#29105,#29106,#29107,#29108,#29109,
#29110,#29111,#29112,#29113,#29114),.UNSPECIFIED.,.F.,.F.,(4,3,3,3,3,3,
3,3,3,3,3,3,3,3,4),(13.8756314554422,14.0631029439831,14.5480375282584,
15.0329721125337,15.5179066968089,16.0028412810842,16.4877758653595,16.9727104496348,
17.45764503391,17.9425796181853,18.4275142024606,18.9124487867359,19.3973833710112,
19.8823179552864,20.1588167626218),.UNSPECIFIED.);
#606=B_SPLINE_CURVE_WITH_KNOTS('',3,(#29115,#29116,#29117,#29118,#29119,
#29120,#29121,#29122,#29123,#29124,#29125,#29126,#29127,#29128,#29129,#29130,
#29131,#29132,#29133,#29134,#29135,#29136,#29137,#29138,#29139,#29140,#29141,
#29142,#29143,#29144,#29145,#29146,#29147,#29148,#29149,#29150,#29151,#29152,
#29153,#29154,#29155,#29156,#29157),.UNSPECIFIED.,.F.,.F.,(4,3,3,3,3,3,
3,3,3,3,3,3,3,3,4),(-16.4222979175632,-16.0028412810842,-15.5179066968089,
-15.0329721125336,-14.5480375282584,-14.0631029439831,-13.5781683597078,
-13.0932337754325,-12.6082991911573,-12.123364606882,-11.6384300226067,
-11.1534954383314,-10.6685608540561,-10.1836262697809,-10.1391126103836),
 .UNSPECIFIED.);
#607=B_SPLINE_CURVE_WITH_KNOTS('',3,(#29163,#29164,#29165,#29166,#29167,
#29168,#29169,#29170,#29171,#29172,#29173,#29174,#29175,#29176,#29177,#29178,
#29179,#29180,#29181,#29182,#29183,#29184,#29185,#29186,#29187),
 .UNSPECIFIED.,.F.,.F.,(4,3,3,3,3,3,3,3,4),(-3.85592730320401,-3.39454208992695,
-2.90960750565167,-2.42467292137639,-1.93973833710111,-1.45480375282584,
-0.969869168550558,-0.484934584275278,0.),.UNSPECIFIED.);
#608=B_SPLINE_CURVE_WITH_KNOTS('',3,(#29190,#29191,#29192,#29193,#29194,
#29195,#29196,#29197,#29198,#29199,#29200,#29201,#29202,#29203,#29204,#29205,
#29206,#29207,#29208,#29209,#29210,#29211,#29212,#29213,#29214,#29215,#29216,
#29217,#29218,#29219,#29220,#29221,#29222,#29223,#29224,#29225,#29226),
 .UNSPECIFIED.,.F.,.F.,(4,3,3,3,3,3,3,3,3,3,3,3,4),(2.02359549069733,2.4246729213764,
2.90960750565168,3.39454208992696,3.87947667420224,4.36441125847751,4.84934584275279,
5.33428042702807,5.81921501130335,6.30414959557863,6.78908417985391,7.27401876412919,
7.59244614826264),.UNSPECIFIED.);
#609=B_SPLINE_CURVE_WITH_KNOTS('',3,(#29232,#29233,#29234,#29235,#29236,
#29237,#29238,#29239,#29240,#29241,#29242,#29243,#29244),.UNSPECIFIED.,
 .F.,.F.,(4,1,1,1,1,1,1,1,1,1,4),(34.5575191894877,34.6439614256831,35.1288960099583,
35.6138305942336,36.0987651785089,36.5836997627842,37.0686343470595,37.5535689313347,
38.03850351561,38.5234380998853,39.0083726841606),.UNSPECIFIED.);
#610=B_SPLINE_CURVE_WITH_KNOTS('',3,(#29247,#29248,#29249,#29250,#29251,
#29252,#29253,#29254,#29255,#29256,#29257,#29258,#29259,#29260),
 .UNSPECIFIED.,.F.,.F.,(4,1,1,1,1,1,1,1,1,1,1,4),(34.5575191894877,34.7659549664276,
35.2508895507029,35.7358241349782,36.2207587192535,36.7056933035287,37.190627887804,
37.6755624720793,38.1604970563546,38.6454316406299,39.1303662249051,39.5314436555842),
 .UNSPECIFIED.);
#611=B_SPLINE_CURVE_WITH_KNOTS('',3,(#29265,#29266,#29267,#29268,#29269,
#29270,#29271,#29272,#29273,#29274,#29275,#29276,#29277,#29278,#29279,#29280,
#29281),.UNSPECIFIED.,.F.,.F.,(4,1,1,1,1,1,1,1,1,1,1,1,1,1,4),(28.2743338823081,
28.3398118301044,28.8247464143797,29.309680998655,29.7946155829303,30.2795501672055,
30.7644847514808,31.2494193357561,31.7343539200314,32.2192885043067,32.7042230885819,
33.1891576728572,33.6740922571325,34.1590268414078,34.5575191894877),
 .UNSPECIFIED.);
#612=B_SPLINE_CURVE_WITH_KNOTS('',3,(#29282,#29283,#29284,#29285,#29286,
#29287,#29288,#29289,#29290,#29291,#29292,#29293,#29294,#29295,#29296,#29297,
#29298),.UNSPECIFIED.,.F.,.F.,(4,1,1,1,1,1,1,1,1,1,1,1,1,1,4),(28.2743338823081,
28.461805370849,28.9467399551243,29.4316745393996,29.9166091236748,30.4015437079501,
30.8864782922254,31.3714128765007,31.856347460776,32.3412820450512,32.8262166293265,
33.3111512136018,33.7960857978771,34.2810203821523,34.5575191894877),
 .UNSPECIFIED.);
#613=B_SPLINE_CURVE_WITH_KNOTS('',3,(#29303,#29304,#29305,#29306,#29307,
#29308,#29309,#29310,#29311,#29312,#29313,#29314,#29315,#29316,#29317,#29318,
#29319),.UNSPECIFIED.,.F.,.F.,(4,1,1,1,1,1,1,1,1,1,1,1,1,1,4),(21.9911485751286,
22.0356622345258,22.5205968188011,23.0055314030764,23.4904659873516,23.9754005716269,
24.4603351559022,24.9452697401775,25.4302043244528,25.915138908728,26.4000734930033,
26.8850080772786,27.3699426615539,27.8548772458292,28.2743338823081),
 .UNSPECIFIED.);
#614=B_SPLINE_CURVE_WITH_KNOTS('',3,(#29320,#29321,#29322,#29323,#29324,
#29325,#29326,#29327,#29328,#29329,#29330,#29331,#29332,#29333,#29334,#29335,
#29336),.UNSPECIFIED.,.F.,.F.,(4,1,1,1,1,1,1,1,1,1,1,1,1,1,4),(21.9911485751286,
22.1576557752704,22.6425903595457,23.1275249438209,23.6124595280962,24.0973941123715,
24.5823286966468,25.067263280922,25.5521978651973,26.0371324494726,26.5220670337479,
27.0070016180232,27.4919362022984,27.9768707865737,28.2743338823081),
 .UNSPECIFIED.);
#615=B_SPLINE_CURVE_WITH_KNOTS('',3,(#29342,#29343,#29344,#29345,#29346,
#29347),.UNSPECIFIED.,.F.,.F.,(4,1,1,4),(14.3987024268659,14.8836370111412,
15.3685715954165,15.707963267949),.UNSPECIFIED.);
#616=B_SPLINE_CURVE_WITH_KNOTS('',3,(#29350,#29351,#29352,#29353,#29354,
#29355,#29356),.UNSPECIFIED.,.F.,.F.,(4,1,1,1,4),(13.8756314554423,14.2767088861213,
14.7616434703966,15.2465780546719,15.707963267949),.UNSPECIFIED.);
#617=B_SPLINE_CURVE_WITH_KNOTS('',3,(#29358,#29359,#29360,#29361,#29362,
#29363,#29364,#29365,#29366,#29367,#29368,#29369,#29370,#29371,#29372,#29373,
#29374),.UNSPECIFIED.,.F.,.F.,(4,1,1,1,1,1,1,1,1,1,1,1,1,1,4),(15.707963267949,
15.7315126389472,16.2164472232225,16.7013818074977,17.186316391773,17.6712509760483,
18.1561855603236,18.6411201445989,19.1260547288741,19.6109893131494,20.0959238974247,
20.5808584817,21.0657930659752,21.5507276502505,21.9911485751286),
 .UNSPECIFIED.);
#618=B_SPLINE_CURVE_WITH_KNOTS('',3,(#29375,#29376,#29377,#29378,#29379,
#29380,#29381,#29382,#29383,#29384,#29385,#29386,#29387,#29388,#29389,#29390,
#29391),.UNSPECIFIED.,.F.,.F.,(4,1,1,1,1,1,1,1,1,1,1,1,1,1,4),(15.707963267949,
15.8535061796917,16.338440763967,16.8233753482423,17.3083099325176,17.7932445167929,
18.2781791010681,18.7631136853434,19.2480482696187,19.732982853894,20.2179174381693,
20.7028520224445,21.1877866067198,21.6727211909951,21.9911485751286),
 .UNSPECIFIED.);
#619=B_SPLINE_CURVE_WITH_KNOTS('',3,(#29628,#29629,#29630,#29631,#29632,
#29633,#29634,#29635,#29636,#29637,#29638,#29639,#29640,#29641,#29642,#29643,
#29644,#29645,#29646,#29647,#29648,#29649,#29650,#29651,#29652,#29653,#29654,
#29655,#29656,#29657,#29658,#29659,#29660,#29661,#29662,#29663,#29664,#29665,
#29666,#29667,#29668,#29669,#29670,#29671,#29672,#29673,#29674,#29675,#29676,
#29677,#29678,#29679,#29680,#29681,#29682,#29683,#29684,#29685,#29686,#29687,
#29688,#29689,#29690,#29691,#29692,#29693,#29694,#29695,#29696,#29697,#29698,
#29699,#29700,#29701,#29702,#29703,#29704,#29705,#29706),.UNSPECIFIED.,
 .F.,.F.,(4,3,3,3,3,3,3,3,3,3,3,3,3,3,3,3,3,3,3,3,3,3,3,3,3,3,4),(0.,0.152217503484067,
0.304359680258418,0.444170485281583,0.471986655324497,0.583981290304748,
0.733405099570558,0.837349441494007,0.892796146824606,0.921013703055727,
0.951233855348084,1.09712094103545,1.14918246726435,1.28571136325166,1.34308233147708,
1.3712989340972,1.51452714133526,1.65613253529925,1.69529805121359,1.76334984211607,
1.7978934044592,1.82919283472952,1.96987767951395,2.04822487844286,2.08147544830853,
2.22116640322431,2.3101075030587),.UNSPECIFIED.);
#620=B_SPLINE_CURVE_WITH_KNOTS('',3,(#29707,#29708,#29709,#29710,#29711,
#29712,#29713,#29714,#29715,#29716,#29717,#29718,#29719,#29720,#29721,#29722,
#29723,#29724,#29725,#29726,#29727,#29728,#29729,#29730,#29731,#29732,#29733,
#29734,#29735,#29736,#29737,#29738,#29739,#29740,#29741,#29742,#29743,#29744,
#29745,#29746,#29747,#29748,#29749,#29750,#29751,#29752,#29753,#29754,#29755,
#29756,#29757,#29758,#29759,#29760,#29761,#29762,#29763,#29764,#29765,#29766,
#29767,#29768,#29769,#29770,#29771,#29772,#29773,#29774,#29775,#29776,#29777,
#29778,#29779,#29780,#29781,#29782),.UNSPECIFIED.,.F.,.F.,(4,3,3,3,3,3,
3,3,3,3,3,3,3,3,3,3,3,3,3,3,3,3,3,3,3,4),(0.,0.136946952689913,0.275845446902835,
0.398834826821011,0.433645114326313,0.521824206739186,0.66322447960231,
0.763149933136536,0.825063822791896,0.861088222426034,1.00600575290352,
1.06292629373921,1.20295657612767,1.26303419900659,1.30095883119802,1.44786439483437,
1.59611049832394,1.62304742329305,1.69648823646563,1.73120190892034,1.76336658984008,
1.91360290275334,1.99760341236776,2.0413262282657,2.20106314648737,2.30292298333826),
 .UNSPECIFIED.);
#621=B_SPLINE_CURVE_WITH_KNOTS('',3,(#29783,#29784,#29785,#29786,#29787,
#29788,#29789,#29790,#29791,#29792,#29793,#29794,#29795,#29796,#29797,#29798,
#29799,#29800,#29801,#29802,#29803,#29804,#29805,#29806,#29807,#29808,#29809,
#29810,#29811,#29812,#29813,#29814,#29815,#29816,#29817,#29818,#29819,#29820,
#29821,#29822,#29823,#29824,#29825),.UNSPECIFIED.,.F.,.F.,(4,3,3,3,3,3,
3,3,3,3,3,3,3,3,4),(-10.1391126103836,-9.69869168550558,-9.2137571012303,
-8.72882251695502,-8.24388793267974,-7.75895334840446,-7.27401876412918,
-6.7890841798539,-6.30414959557862,-5.81921501130335,-5.33428042702807,
-4.84934584275279,-4.36441125847751,-3.87947667420223,-3.85592730320401),
 .UNSPECIFIED.);
#622=B_SPLINE_CURVE_WITH_KNOTS('',3,(#30062,#30063,#30064,#30065,#30066,
#30067,#30068,#30069,#30070,#30071,#30072,#30073,#30074,#30075,#30076,#30077,
#30078,#30079,#30080,#30081,#30082,#30083,#30084,#30085,#30086,#30087,#30088,
#30089,#30090,#30091,#30092,#30093,#30094,#30095,#30096,#30097,#30098,#30099,
#30100,#30101,#30102,#30103,#30104,#30105,#30106,#30107,#30108,#30109,#30110,
#30111,#30112,#30113,#30114,#30115,#30116,#30117,#30118,#30119,#30120,#30121,
#30122,#30123,#30124,#30125,#30126,#30127,#30128,#30129,#30130,#30131,#30132,
#30133,#30134,#30135,#30136,#30137),.UNSPECIFIED.,.F.,.F.,(4,3,3,3,3,3,
3,3,3,3,3,3,3,3,3,3,3,3,3,3,3,3,3,3,3,4),(0.,0.136946810378538,0.275845240706276,
0.398834723722739,0.4336450955117,0.521824206739202,0.663224551971021,0.763149987413078,
0.825063985186383,0.861088231251125,1.00600581272087,1.06292629373925,1.20295657612771,
1.26303419911027,1.30095883168088,1.44786437076391,1.59611047038881,1.6230474232931,
1.69648823731838,1.7312019179875,1.76336659191163,1.9136029038652,1.9976034144013,
2.04132622941513,2.20106314648744,2.30292298333833),.UNSPECIFIED.);
#623=B_SPLINE_CURVE_WITH_KNOTS('',3,(#30138,#30139,#30140,#30141,#30142,
#30143,#30144,#30145,#30146,#30147,#30148,#30149,#30150,#30151,#30152,#30153,
#30154,#30155,#30156,#30157,#30158,#30159,#30160,#30161,#30162,#30163,#30164,
#30165,#30166,#30167,#30168,#30169,#30170,#30171,#30172,#30173,#30174,#30175,
#30176,#30177,#30178,#30179,#30180),.UNSPECIFIED.,.F.,.F.,(4,3,3,3,3,3,
3,3,3,3,3,3,3,3,4),(7.59244614826264,7.75895334840446,8.24388793267975,
8.72882251695503,9.21375710123031,9.69869168550558,10.1836262697809,10.6685608540561,
11.1534954383314,11.6384300226067,12.123364606882,12.6082991911573,13.0932337754325,
13.5781683597078,13.8756314554422),.UNSPECIFIED.);
#624=B_SPLINE_CURVE_WITH_KNOTS('',3,(#30181,#30182,#30183,#30184,#30185,
#30186,#30187,#30188,#30189,#30190,#30191,#30192,#30193,#30194,#30195,#30196,
#30197,#30198,#30199,#30200,#30201,#30202,#30203,#30204,#30205,#30206,#30207,
#30208,#30209,#30210,#30211,#30212,#30213,#30214,#30215,#30216,#30217,#30218,
#30219,#30220,#30221,#30222,#30223,#30224,#30225,#30226,#30227,#30228,#30229,
#30230,#30231,#30232,#30233,#30234,#30235,#30236,#30237,#30238,#30239,#30240,
#30241,#30242,#30243,#30244,#30245,#30246,#30247,#30248,#30249,#30250,#30251,
#30252,#30253,#30254,#30255,#30256,#30257,#30258,#30259),.UNSPECIFIED.,
 .F.,.F.,(4,3,3,3,3,3,3,3,3,3,3,3,3,3,3,3,3,3,3,3,3,3,3,3,3,3,4),(0.,0.152217449424706,
0.304359666709038,0.444170478506893,0.471986651289376,0.583981290304748,
0.733405107154758,0.837349447182159,0.892796173398726,0.921013624406268,
0.951233846940009,1.09712092482237,1.14918246726436,1.28571136325167,1.34308233538123,
1.37129893684867,1.51452714023172,1.65613252898941,1.6952980512136,1.76334984315127,
1.79789341460453,1.829192837075,1.96987768339371,2.04822488467355,2.08147545454654,
2.22116640322432,2.3101075030587),.UNSPECIFIED.);
#715=SHAPE_REPRESENTATION_RELATIONSHIP('SRR','None',#34558,#737);
#737=ADVANCED_BREP_SHAPE_REPRESENTATION('',(#795),#34426);
#767=STYLED_ITEM('',(#34750),#795);
#795=MANIFOLD_SOLID_BREP('Body1',#8796);
#849=FACE_BOUND('',#2000,.T.);
#850=FACE_BOUND('',#2009,.T.);
#1012=PLANE('',#9635);
#1013=PLANE('',#9637);
#1014=PLANE('',#9638);
#1015=PLANE('',#9639);
#1016=PLANE('',#9640);
#1017=PLANE('',#9641);
#1018=PLANE('',#9642);
#1019=PLANE('',#9643);
#1451=FACE_OUTER_BOUND('',#1988,.T.);
#1452=FACE_OUTER_BOUND('',#1989,.T.);
#1453=FACE_OUTER_BOUND('',#1990,.T.);
#1454=FACE_OUTER_BOUND('',#1991,.T.);
#1455=FACE_OUTER_BOUND('',#1992,.T.);
#1456=FACE_OUTER_BOUND('',#1993,.T.);
#1457=FACE_OUTER_BOUND('',#1994,.T.);
#1458=FACE_OUTER_BOUND('',#1995,.T.);
#1459=FACE_OUTER_BOUND('',#1996,.T.);
#1460=FACE_OUTER_BOUND('',#1997,.T.);
#1461=FACE_OUTER_BOUND('',#1998,.T.);
#1462=FACE_OUTER_BOUND('',#1999,.T.);
#1463=FACE_OUTER_BOUND('',#2001,.T.);
#1464=FACE_OUTER_BOUND('',#2002,.T.);
#1465=FACE_OUTER_BOUND('',#2003,.T.);
#1466=FACE_OUTER_BOUND('',#2004,.T.);
#1467=FACE_OUTER_BOUND('',#2005,.T.);
#1468=FACE_OUTER_BOUND('',#2006,.T.);
#1469=FACE_OUTER_BOUND('',#2007,.T.);
#1470=FACE_OUTER_BOUND('',#2008,.T.);
#1988=EDGE_LOOP('',(#7567,#7568,#7569,#7570));
#1989=EDGE_LOOP('',(#7571,#7572,#7573,#7574));
#1990=EDGE_LOOP('',(#7575,#7576,#7577,#7578));
#1991=EDGE_LOOP('',(#7579,#7580,#7581,#7582));
#1992=EDGE_LOOP('',(#7583,#7584,#7585,#7586));
#1993=EDGE_LOOP('',(#7587,#7588,#7589,#7590));
#1994=EDGE_LOOP('',(#7591,#7592,#7593,#7594));
#1995=EDGE_LOOP('',(#7595,#7596,#7597,#7598));
#1996=EDGE_LOOP('',(#7599,#7600,#7601,#7602));
#1997=EDGE_LOOP('',(#7603,#7604,#7605,#7606,#7607,#7608,#7609,#7610,#7611,
#7612,#7613,#7614));
#1998=EDGE_LOOP('',(#7615,#7616,#7617,#7618,#7619,#7620,#7621,#7622,#7623,
#7624,#7625,#7626));
#1999=EDGE_LOOP('',(#7627,#7628,#7629,#7630,#7631,#7632));
#2000=EDGE_LOOP('',(#7633,#7634,#7635,#7636));
#2001=EDGE_LOOP('',(#7637,#7638,#7639,#7640));
#2002=EDGE_LOOP('',(#7641,#7642,#7643,#7644));
#2003=EDGE_LOOP('',(#7645,#7646,#7647,#7648));
#2004=EDGE_LOOP('',(#7649,#7650,#7651,#7652));
#2005=EDGE_LOOP('',(#7653,#7654,#7655,#7656));
#2006=EDGE_LOOP('',(#7657,#7658,#7659,#7660));
#2007=EDGE_LOOP('',(#7661,#7662,#7663,#7664));
#2008=EDGE_LOOP('',(#7665,#7666,#7667,#7668,#7669,#7670));
#2009=EDGE_LOOP('',(#7671,#7672,#7673,#7674));
#2589=LINE('',#28948,#3206);
#2590=LINE('',#28981,#3207);
#2591=LINE('',#29071,#3208);
#2592=LINE('',#29161,#3209);
#2593=LINE('',#29230,#3210);
#2594=LINE('',#29264,#3211);
#2595=LINE('',#29302,#3212);
#2596=LINE('',#29340,#3213);
#2597=LINE('',#30263,#3214);
#2598=LINE('',#30265,#3215);
#2599=LINE('',#30267,#3216);
#2600=LINE('',#30269,#3217);
#2601=LINE('',#30271,#3218);
#2602=LINE('',#30272,#3219);
#2603=LINE('',#30277,#3220);
#2604=LINE('',#30278,#3221);
#2605=LINE('',#30279,#3222);
#2606=LINE('',#30282,#3223);
#2607=LINE('',#30283,#3224);
#2608=LINE('',#30286,#3225);
#2609=LINE('',#30287,#3226);
#2610=LINE('',#30290,#3227);
#2611=LINE('',#30291,#3228);
#2612=LINE('',#30294,#3229);
#2613=LINE('',#30295,#3230);
#2614=LINE('',#30297,#3231);
#3206=VECTOR('',#11398,1.05);
#3207=VECTOR('',#11403,1.05);
#3208=VECTOR('',#11406,1.05);
#3209=VECTOR('',#11409,1.05);
#3210=VECTOR('',#11414,1.21745);
#3211=VECTOR('',#11419,1.21745);
#3212=VECTOR('',#11422,1.21745);
#3213=VECTOR('',#11425,1.21745);
#3214=VECTOR('',#11432,1.);
#3215=VECTOR('',#11433,1.);
#3216=VECTOR('',#11434,1.);
#3217=VECTOR('',#11435,1.);
#3218=VECTOR('',#11436,1.);
#3219=VECTOR('',#11437,1.);
#3220=VECTOR('',#11442,1.);
#3221=VECTOR('',#11443,1.);
#3222=VECTOR('',#11444,1.);
#3223=VECTOR('',#11447,1.);
#3224=VECTOR('',#11448,1.);
#3225=VECTOR('',#11451,1.);
#3226=VECTOR('',#11452,1.);
#3227=VECTOR('',#11455,1.);
#3228=VECTOR('',#11456,1.);
#3229=VECTOR('',#11459,1.);
#3230=VECTOR('',#11460,1.);
#3231=VECTOR('',#11463,1.);
#3428=CIRCLE('',#9623,1.0501);
#3429=CIRCLE('',#9627,1.0501);
#3430=CIRCLE('',#9629,1.21745);
#3431=CIRCLE('',#9633,1.21745);
#4126=VERTEX_POINT('',#28946);
#4127=VERTEX_POINT('',#28947);
#4128=VERTEX_POINT('',#28949);
#4129=VERTEX_POINT('',#28957);
#4130=VERTEX_POINT('',#28979);
#4131=VERTEX_POINT('',#28980);
#4132=VERTEX_POINT('',#29069);
#4133=VERTEX_POINT('',#29070);
#4134=VERTEX_POINT('',#29159);
#4135=VERTEX_POINT('',#29160);
#4136=VERTEX_POINT('',#29162);
#4137=VERTEX_POINT('',#29188);
#4138=VERTEX_POINT('',#29228);
#4139=VERTEX_POINT('',#29229);
#4140=VERTEX_POINT('',#29231);
#4141=VERTEX_POINT('',#29245);
#4142=VERTEX_POINT('',#29262);
#4143=VERTEX_POINT('',#29263);
#4144=VERTEX_POINT('',#29300);
#4145=VERTEX_POINT('',#29301);
#4146=VERTEX_POINT('',#29338);
#4147=VERTEX_POINT('',#29339);
#4148=VERTEX_POINT('',#29341);
#4149=VERTEX_POINT('',#29348);
#4150=VERTEX_POINT('',#30261);
#4151=VERTEX_POINT('',#30262);
#4152=VERTEX_POINT('',#30264);
#4153=VERTEX_POINT('',#30266);
#4154=VERTEX_POINT('',#30268);
#4155=VERTEX_POINT('',#30270);
#4156=VERTEX_POINT('',#30275);
#4157=VERTEX_POINT('',#30276);
#4158=VERTEX_POINT('',#30281);
#4159=VERTEX_POINT('',#30285);
#4160=VERTEX_POINT('',#30289);
#4161=VERTEX_POINT('',#30293);
#5297=EDGE_CURVE('',#4126,#4127,#2589,.T.);
#5298=EDGE_CURVE('',#4127,#4128,#601,.T.);
#5299=EDGE_CURVE('',#4129,#4128,#3428,.T.);
#5300=EDGE_CURVE('',#4129,#4126,#602,.T.);
#5301=EDGE_CURVE('',#4130,#4131,#2590,.T.);
#5302=EDGE_CURVE('',#4131,#4127,#603,.T.);
#5303=EDGE_CURVE('',#4126,#4130,#604,.T.);
#5304=EDGE_CURVE('',#4132,#4133,#2591,.T.);
#5305=EDGE_CURVE('',#4133,#4131,#605,.T.);
#5306=EDGE_CURVE('',#4130,#4132,#606,.T.);
#5307=EDGE_CURVE('',#4134,#4135,#2592,.T.);
#5308=EDGE_CURVE('',#4134,#4136,#607,.T.);
#5309=EDGE_CURVE('',#4137,#4136,#3429,.F.);
#5310=EDGE_CURVE('',#4137,#4135,#608,.T.);
#5311=EDGE_CURVE('',#4138,#4139,#2593,.T.);
#5312=EDGE_CURVE('',#4139,#4140,#609,.T.);
#5313=EDGE_CURVE('',#4141,#4140,#3430,.T.);
#5314=EDGE_CURVE('',#4138,#4141,#610,.T.);
#5315=EDGE_CURVE('',#4142,#4143,#2594,.T.);
#5316=EDGE_CURVE('',#4143,#4139,#611,.T.);
#5317=EDGE_CURVE('',#4142,#4138,#612,.T.);
#5318=EDGE_CURVE('',#4144,#4145,#2595,.T.);
#5319=EDGE_CURVE('',#4145,#4143,#613,.T.);
#5320=EDGE_CURVE('',#4144,#4142,#614,.T.);
#5321=EDGE_CURVE('',#4146,#4147,#2596,.T.);
#5322=EDGE_CURVE('',#4148,#4146,#615,.T.);
#5323=EDGE_CURVE('',#4149,#4148,#3431,.T.);
#5324=EDGE_CURVE('',#4149,#4147,#616,.T.);
#5325=EDGE_CURVE('',#4147,#4145,#617,.T.);
#5326=EDGE_CURVE('',#4146,#4144,#618,.T.);
#5327=EDGE_CURVE('',#4140,#4129,#619,.T.);
#5328=EDGE_CURVE('',#4136,#4149,#620,.T.);
#5329=EDGE_CURVE('',#4132,#4134,#621,.T.);
#5330=EDGE_CURVE('',#4128,#4141,#622,.T.);
#5331=EDGE_CURVE('',#4135,#4133,#623,.T.);
#5332=EDGE_CURVE('',#4148,#4137,#624,.T.);
#5333=EDGE_CURVE('',#4150,#4151,#2597,.T.);
#5334=EDGE_CURVE('',#4151,#4152,#2598,.T.);
#5335=EDGE_CURVE('',#4152,#4153,#2599,.T.);
#5336=EDGE_CURVE('',#4153,#4154,#2600,.T.);
#5337=EDGE_CURVE('',#4154,#4155,#2601,.T.);
#5338=EDGE_CURVE('',#4155,#4150,#2602,.T.);
#5339=EDGE_CURVE('',#4156,#4157,#2603,.T.);
#5340=EDGE_CURVE('',#4157,#4150,#2604,.T.);
#5341=EDGE_CURVE('',#4156,#4155,#2605,.T.);
#5342=EDGE_CURVE('',#4158,#4156,#2606,.T.);
#5343=EDGE_CURVE('',#4158,#4154,#2607,.T.);
#5344=EDGE_CURVE('',#4159,#4158,#2608,.T.);
#5345=EDGE_CURVE('',#4159,#4153,#2609,.T.);
#5346=EDGE_CURVE('',#4160,#4159,#2610,.T.);
#5347=EDGE_CURVE('',#4160,#4152,#2611,.T.);
#5348=EDGE_CURVE('',#4161,#4160,#2612,.T.);
#5349=EDGE_CURVE('',#4161,#4151,#2613,.T.);
#5350=EDGE_CURVE('',#4157,#4161,#2614,.T.);
#7567=ORIENTED_EDGE('',*,*,#5297,.T.);
#7568=ORIENTED_EDGE('',*,*,#5298,.T.);
#7569=ORIENTED_EDGE('',*,*,#5299,.F.);
#7570=ORIENTED_EDGE('',*,*,#5300,.T.);
#7571=ORIENTED_EDGE('',*,*,#5301,.T.);
#7572=ORIENTED_EDGE('',*,*,#5302,.T.);
#7573=ORIENTED_EDGE('',*,*,#5297,.F.);
#7574=ORIENTED_EDGE('',*,*,#5303,.T.);
#7575=ORIENTED_EDGE('',*,*,#5304,.T.);
#7576=ORIENTED_EDGE('',*,*,#5305,.T.);
#7577=ORIENTED_EDGE('',*,*,#5301,.F.);
#7578=ORIENTED_EDGE('',*,*,#5306,.T.);
#7579=ORIENTED_EDGE('',*,*,#5307,.F.);
#7580=ORIENTED_EDGE('',*,*,#5308,.T.);
#7581=ORIENTED_EDGE('',*,*,#5309,.F.);
#7582=ORIENTED_EDGE('',*,*,#5310,.T.);
#7583=ORIENTED_EDGE('',*,*,#5311,.T.);
#7584=ORIENTED_EDGE('',*,*,#5312,.T.);
#7585=ORIENTED_EDGE('',*,*,#5313,.F.);
#7586=ORIENTED_EDGE('',*,*,#5314,.F.);
#7587=ORIENTED_EDGE('',*,*,#5315,.T.);
#7588=ORIENTED_EDGE('',*,*,#5316,.T.);
#7589=ORIENTED_EDGE('',*,*,#5311,.F.);
#7590=ORIENTED_EDGE('',*,*,#5317,.F.);
#7591=ORIENTED_EDGE('',*,*,#5318,.T.);
#7592=ORIENTED_EDGE('',*,*,#5319,.T.);
#7593=ORIENTED_EDGE('',*,*,#5315,.F.);
#7594=ORIENTED_EDGE('',*,*,#5320,.F.);
#7595=ORIENTED_EDGE('',*,*,#5321,.F.);
#7596=ORIENTED_EDGE('',*,*,#5322,.F.);
#7597=ORIENTED_EDGE('',*,*,#5323,.F.);
#7598=ORIENTED_EDGE('',*,*,#5324,.T.);
#7599=ORIENTED_EDGE('',*,*,#5321,.T.);
#7600=ORIENTED_EDGE('',*,*,#5325,.T.);
#7601=ORIENTED_EDGE('',*,*,#5318,.F.);
#7602=ORIENTED_EDGE('',*,*,#5326,.F.);
#7603=ORIENTED_EDGE('',*,*,#5327,.F.);
#7604=ORIENTED_EDGE('',*,*,#5312,.F.);
#7605=ORIENTED_EDGE('',*,*,#5316,.F.);
#7606=ORIENTED_EDGE('',*,*,#5319,.F.);
#7607=ORIENTED_EDGE('',*,*,#5325,.F.);
#7608=ORIENTED_EDGE('',*,*,#5324,.F.);
#7609=ORIENTED_EDGE('',*,*,#5328,.F.);
#7610=ORIENTED_EDGE('',*,*,#5308,.F.);
#7611=ORIENTED_EDGE('',*,*,#5329,.F.);
#7612=ORIENTED_EDGE('',*,*,#5306,.F.);
#7613=ORIENTED_EDGE('',*,*,#5303,.F.);
#7614=ORIENTED_EDGE('',*,*,#5300,.F.);
#7615=ORIENTED_EDGE('',*,*,#5330,.F.);
#7616=ORIENTED_EDGE('',*,*,#5298,.F.);
#7617=ORIENTED_EDGE('',*,*,#5302,.F.);
#7618=ORIENTED_EDGE('',*,*,#5305,.F.);
#7619=ORIENTED_EDGE('',*,*,#5331,.F.);
#7620=ORIENTED_EDGE('',*,*,#5310,.F.);
#7621=ORIENTED_EDGE('',*,*,#5332,.F.);
#7622=ORIENTED_EDGE('',*,*,#5322,.T.);
#7623=ORIENTED_EDGE('',*,*,#5326,.T.);
#7624=ORIENTED_EDGE('',*,*,#5320,.T.);
#7625=ORIENTED_EDGE('',*,*,#5317,.T.);
#7626=ORIENTED_EDGE('',*,*,#5314,.T.);
#7627=ORIENTED_EDGE('',*,*,#5333,.T.);
#7628=ORIENTED_EDGE('',*,*,#5334,.T.);
#7629=ORIENTED_EDGE('',*,*,#5335,.T.);
#7630=ORIENTED_EDGE('',*,*,#5336,.T.);
#7631=ORIENTED_EDGE('',*,*,#5337,.T.);
#7632=ORIENTED_EDGE('',*,*,#5338,.T.);
#7633=ORIENTED_EDGE('',*,*,#5330,.T.);
#7634=ORIENTED_EDGE('',*,*,#5313,.T.);
#7635=ORIENTED_EDGE('',*,*,#5327,.T.);
#7636=ORIENTED_EDGE('',*,*,#5299,.T.);
#7637=ORIENTED_EDGE('',*,*,#5307,.T.);
#7638=ORIENTED_EDGE('',*,*,#5331,.T.);
#7639=ORIENTED_EDGE('',*,*,#5304,.F.);
#7640=ORIENTED_EDGE('',*,*,#5329,.T.);
#7641=ORIENTED_EDGE('',*,*,#5339,.T.);
#7642=ORIENTED_EDGE('',*,*,#5340,.T.);
#7643=ORIENTED_EDGE('',*,*,#5338,.F.);
#7644=ORIENTED_EDGE('',*,*,#5341,.F.);
#7645=ORIENTED_EDGE('',*,*,#5342,.T.);
#7646=ORIENTED_EDGE('',*,*,#5341,.T.);
#7647=ORIENTED_EDGE('',*,*,#5337,.F.);
#7648=ORIENTED_EDGE('',*,*,#5343,.F.);
#7649=ORIENTED_EDGE('',*,*,#5344,.T.);
#7650=ORIENTED_EDGE('',*,*,#5343,.T.);
#7651=ORIENTED_EDGE('',*,*,#5336,.F.);
#7652=ORIENTED_EDGE('',*,*,#5345,.F.);
#7653=ORIENTED_EDGE('',*,*,#5346,.T.);
#7654=ORIENTED_EDGE('',*,*,#5345,.T.);
#7655=ORIENTED_EDGE('',*,*,#5335,.F.);
#7656=ORIENTED_EDGE('',*,*,#5347,.F.);
#7657=ORIENTED_EDGE('',*,*,#5348,.T.);
#7658=ORIENTED_EDGE('',*,*,#5347,.T.);
#7659=ORIENTED_EDGE('',*,*,#5334,.F.);
#7660=ORIENTED_EDGE('',*,*,#5349,.F.);
#7661=ORIENTED_EDGE('',*,*,#5350,.T.);
#7662=ORIENTED_EDGE('',*,*,#5349,.T.);
#7663=ORIENTED_EDGE('',*,*,#5333,.F.);
#7664=ORIENTED_EDGE('',*,*,#5340,.F.);
#7665=ORIENTED_EDGE('',*,*,#5350,.F.);
#7666=ORIENTED_EDGE('',*,*,#5339,.F.);
#7667=ORIENTED_EDGE('',*,*,#5342,.F.);
#7668=ORIENTED_EDGE('',*,*,#5344,.F.);
#7669=ORIENTED_EDGE('',*,*,#5346,.F.);
#7670=ORIENTED_EDGE('',*,*,#5348,.F.);
#7671=ORIENTED_EDGE('',*,*,#5332,.T.);
#7672=ORIENTED_EDGE('',*,*,#5309,.T.);
#7673=ORIENTED_EDGE('',*,*,#5328,.T.);
#7674=ORIENTED_EDGE('',*,*,#5323,.T.);
#8241=CYLINDRICAL_SURFACE('',#9622,1.0501);
#8242=CYLINDRICAL_SURFACE('',#9624,1.0501);
#8243=CYLINDRICAL_SURFACE('',#9625,1.0501);
#8244=CYLINDRICAL_SURFACE('',#9626,1.0501);
#8245=CYLINDRICAL_SURFACE('',#9628,1.21745);
#8246=CYLINDRICAL_SURFACE('',#9630,1.21745);
#8247=CYLINDRICAL_SURFACE('',#9631,1.21745);
#8248=CYLINDRICAL_SURFACE('',#9632,1.21745);
#8249=CYLINDRICAL_SURFACE('',#9634,1.21745);
#8250=CYLINDRICAL_SURFACE('',#9636,1.0501);
#8688=ADVANCED_FACE('',(#1451),#8241,.F.);
#8689=ADVANCED_FACE('',(#1452),#8242,.F.);
#8690=ADVANCED_FACE('',(#1453),#8243,.F.);
#8691=ADVANCED_FACE('',(#1454),#8244,.F.);
#8692=ADVANCED_FACE('',(#1455),#8245,.F.);
#8693=ADVANCED_FACE('',(#1456),#8246,.F.);
#8694=ADVANCED_FACE('',(#1457),#8247,.F.);
#8695=ADVANCED_FACE('',(#1458),#8248,.F.);
#8696=ADVANCED_FACE('',(#1459),#8249,.F.);
#8697=ADVANCED_FACE('',(#1460),#209,.F.);
#8698=ADVANCED_FACE('',(#1461),#210,.F.);
#8699=ADVANCED_FACE('',(#1462,#849),#1012,.T.);
#8700=ADVANCED_FACE('',(#1463),#8250,.F.);
#8701=ADVANCED_FACE('',(#1464),#1013,.T.);
#8702=ADVANCED_FACE('',(#1465),#1014,.T.);
#8703=ADVANCED_FACE('',(#1466),#1015,.T.);
#8704=ADVANCED_FACE('',(#1467),#1016,.T.);
#8705=ADVANCED_FACE('',(#1468),#1017,.T.);
#8706=ADVANCED_FACE('',(#1469),#1018,.T.);
#8707=ADVANCED_FACE('',(#1470,#850),#1019,.F.);
#8796=CLOSED_SHELL('',(#8688,#8689,#8690,#8691,#8692,#8693,#8694,#8695,
#8696,#8697,#8698,#8699,#8700,#8701,#8702,#8703,#8704,#8705,#8706,#8707));
#9621=AXIS2_PLACEMENT_3D('',#28944,#11394,#11395);
#9622=AXIS2_PLACEMENT_3D('',#28945,#11396,#11397);
#9623=AXIS2_PLACEMENT_3D('',#28958,#11399,#11400);
#9624=AXIS2_PLACEMENT_3D('',#28978,#11401,#11402);
#9625=AXIS2_PLACEMENT_3D('',#29068,#11404,#11405);
#9626=AXIS2_PLACEMENT_3D('',#29158,#11407,#11408);
#9627=AXIS2_PLACEMENT_3D('',#29189,#11410,#11411);
#9628=AXIS2_PLACEMENT_3D('',#29227,#11412,#11413);
#9629=AXIS2_PLACEMENT_3D('',#29246,#11415,#11416);
#9630=AXIS2_PLACEMENT_3D('',#29261,#11417,#11418);
#9631=AXIS2_PLACEMENT_3D('',#29299,#11420,#11421);
#9632=AXIS2_PLACEMENT_3D('',#29337,#11423,#11424);
#9633=AXIS2_PLACEMENT_3D('',#29349,#11426,#11427);
#9634=AXIS2_PLACEMENT_3D('',#29357,#11428,#11429);
#9635=AXIS2_PLACEMENT_3D('',#30260,#11430,#11431);
#9636=AXIS2_PLACEMENT_3D('',#30273,#11438,#11439);
#9637=AXIS2_PLACEMENT_3D('',#30274,#11440,#11441);
#9638=AXIS2_PLACEMENT_3D('',#30280,#11445,#11446);
#9639=AXIS2_PLACEMENT_3D('',#30284,#11449,#11450);
#9640=AXIS2_PLACEMENT_3D('',#30288,#11453,#11454);
#9641=AXIS2_PLACEMENT_3D('',#30292,#11457,#11458);
#9642=AXIS2_PLACEMENT_3D('',#30296,#11461,#11462);
#9643=AXIS2_PLACEMENT_3D('',#30298,#11464,#11465);
#11394=DIRECTION('axis',(0.,0.,1.));
#11395=DIRECTION('refdir',(1.,0.,0.));
#11396=DIRECTION('center_axis',(0.,0.,1.));
#11397=DIRECTION('ref_axis',(1.,0.,0.));
#11398=DIRECTION('',(0.,0.,1.));
#11399=DIRECTION('center_axis',(0.,0.,-1.));
#11400=DIRECTION('ref_axis',(1.,0.,0.));
#11401=DIRECTION('center_axis',(0.,0.,1.));
#11402=DIRECTION('ref_axis',(1.,0.,0.));
#11403=DIRECTION('',(0.,0.,1.));
#11404=DIRECTION('center_axis',(0.,0.,1.));
#11405=DIRECTION('ref_axis',(1.,0.,0.));
#11406=DIRECTION('',(0.,0.,1.));
#11407=DIRECTION('center_axis',(0.,0.,1.));
#11408=DIRECTION('ref_axis',(0.936891289691661,0.349620810736282,0.));
#11409=DIRECTION('',(0.,0.,1.));
#11410=DIRECTION('center_axis',(0.,0.,-1.));
#11411=DIRECTION('ref_axis',(1.,0.,0.));
#11412=DIRECTION('center_axis',(0.,0.,1.));
#11413=DIRECTION('ref_axis',(1.,-1.39727864928002E-15,0.));
#11414=DIRECTION('',(1.22464679914735E-16,-1.56119684709152E-31,1.));
#11415=DIRECTION('center_axis',(0.,0.,-1.));
#11416=DIRECTION('ref_axis',(1.,-1.39727864928002E-15,0.));
#11417=DIRECTION('center_axis',(0.,0.,1.));
#11418=DIRECTION('ref_axis',(1.,-1.39727864928002E-15,0.));
#11419=DIRECTION('',(1.22464679914735E-16,-1.56119684709152E-31,1.));
#11420=DIRECTION('center_axis',(0.,0.,1.));
#11421=DIRECTION('ref_axis',(1.,-1.39727864928002E-15,0.));
#11422=DIRECTION('',(1.22464679914735E-16,-1.56119684709152E-31,1.));
#11423=DIRECTION('center_axis',(0.,0.,1.));
#11424=DIRECTION('ref_axis',(-0.608867739087164,0.79327175438111,0.));
#11425=DIRECTION('',(1.22464679914735E-16,-1.56119684709152E-31,1.));
#11426=DIRECTION('center_axis',(0.,0.,1.));
#11427=DIRECTION('ref_axis',(1.,-1.39727864928002E-15,0.));
#11428=DIRECTION('center_axis',(0.,0.,1.));
#11429=DIRECTION('ref_axis',(1.,-1.39727864928002E-15,0.));
#11430=DIRECTION('center_axis',(0.,0.,1.));
#11431=DIRECTION('ref_axis',(1.,0.,0.));
#11432=DIRECTION('',(0.5,0.866025403784439,0.));
#11433=DIRECTION('',(-0.5,0.866025403784439,0.));
#11434=DIRECTION('',(-1.,0.,0.));
#11435=DIRECTION('',(-0.5,-0.866025403784439,0.));
#11436=DIRECTION('',(0.499999999999999,-0.866025403784439,0.));
#11437=DIRECTION('',(1.,-2.13662520709285E-16,0.));
#11438=DIRECTION('center_axis',(0.,0.,1.));
#11439=DIRECTION('ref_axis',(1.,0.,0.));
#11440=DIRECTION('center_axis',(-2.13662520709285E-16,-1.,0.));
#11441=DIRECTION('ref_axis',(1.,-2.13662520709285E-16,0.));
#11442=DIRECTION('',(1.,-2.13662520709285E-16,0.));
#11443=DIRECTION('',(0.,0.,1.));
#11444=DIRECTION('',(0.,0.,1.));
#11445=DIRECTION('center_axis',(-0.866025403784439,-0.499999999999999,0.));
#11446=DIRECTION('ref_axis',(0.499999999999999,-0.866025403784439,0.));
#11447=DIRECTION('',(0.499999999999999,-0.866025403784439,0.));
#11448=DIRECTION('',(0.,0.,1.));
#11449=DIRECTION('center_axis',(-0.866025403784439,0.5,0.));
#11450=DIRECTION('ref_axis',(-0.5,-0.866025403784439,0.));
#11451=DIRECTION('',(-0.5,-0.866025403784439,0.));
#11452=DIRECTION('',(0.,0.,1.));
#11453=DIRECTION('center_axis',(0.,1.,0.));
#11454=DIRECTION('ref_axis',(-1.,0.,0.));
#11455=DIRECTION('',(-1.,0.,0.));
#11456=DIRECTION('',(0.,0.,1.));
#11457=DIRECTION('center_axis',(0.866025403784439,0.5,0.));
#11458=DIRECTION('ref_axis',(-0.5,0.866025403784439,0.));
#11459=DIRECTION('',(-0.5,0.866025403784439,0.));
#11460=DIRECTION('',(0.,0.,1.));
#11461=DIRECTION('center_axis',(0.866025403784439,-0.5,0.));
#11462=DIRECTION('ref_axis',(0.5,0.866025403784439,0.));
#11463=DIRECTION('',(0.5,0.866025403784439,0.));
#11464=DIRECTION('center_axis',(0.,0.,1.));
#11465=DIRECTION('ref_axis',(1.,0.,0.));
#28944=CARTESIAN_POINT('',(0.,0.,0.));
#28945=CARTESIAN_POINT('Origin',(-8.5,0.,13.7));
#28946=CARTESIAN_POINT('',(-9.55012781659967,-2.18430157070126E-5,14.8841069671524));
#28947=CARTESIAN_POINT('',(-9.55001141291652,-2.01662567329067E-6,14.9658930328476));
#28948=CARTESIAN_POINT('',(-9.5501,-1.28600160378464E-16,13.7));
#28949=CARTESIAN_POINT('',(-9.29338130674009,-0.687936125025709,15.));
#28950=CARTESIAN_POINT('Ctrl Pts',(-9.55001141291652,-2.01662567329067E-6,
14.9658930328476));
#28951=CARTESIAN_POINT('Ctrl Pts',(-9.55001922277969,-0.0803165835301839,
14.9695440482821));
#28952=CARTESIAN_POINT('Ctrl Pts',(-9.54090778743713,-0.160626033963762,
14.9731950637165));
#28953=CARTESIAN_POINT('Ctrl Pts',(-9.52264958339625,-0.238792272757937,
14.9768460791509));
#28954=CARTESIAN_POINT('Ctrl Pts',(-9.48405310534775,-0.404029856531109,
14.9845640527673));
#28955=CARTESIAN_POINT('Ctrl Pts',(-9.40458264633919,-0.559690113640443,
14.9922820263836));
#28956=CARTESIAN_POINT('Ctrl Pts',(-9.2933813067401,-0.687936125025703,
15.));
#28957=CARTESIAN_POINT('',(-7.70661869325995,-0.687936125025756,15.));
#28958=CARTESIAN_POINT('Origin',(-8.5,0.,15.));
#28959=CARTESIAN_POINT('Ctrl Pts',(-7.70658096099556,-0.687940818620804,
15.));
#28960=CARTESIAN_POINT('Ctrl Pts',(-7.79864161971976,-0.793915406016005,
14.9936166544345));
#28961=CARTESIAN_POINT('Ctrl Pts',(-7.91206836837192,-0.881430565297469,
14.987233308869));
#28962=CARTESIAN_POINT('Ctrl Pts',(-8.03812224866575,-0.943160376009438,
14.9808499633034));
#28963=CARTESIAN_POINT('Ctrl Pts',(-8.1905314379165,-1.01779663775151,14.9731319896871));
#28964=CARTESIAN_POINT('Ctrl Pts',(-8.36139989944402,-1.05473797530154,
14.9654140160707));
#28965=CARTESIAN_POINT('Ctrl Pts',(-8.53102861693969,-1.04972405688955,
14.9576960424544));
#28966=CARTESIAN_POINT('Ctrl Pts',(-8.70065733443535,-1.04471013847756,
14.949978068838));
#28967=CARTESIAN_POINT('Ctrl Pts',(-8.86904630789917,-0.997740964103553,
14.9422600952216));
#28968=CARTESIAN_POINT('Ctrl Pts',(-9.01678065422342,-0.914232359021707,
14.9345421216053));
#28969=CARTESIAN_POINT('Ctrl Pts',(-9.16451500054767,-0.830723753939859,
14.9268241479889));
#28970=CARTESIAN_POINT('Ctrl Pts',(-9.29159471973234,-0.710675718150169,
14.9191061743726));
#28971=CARTESIAN_POINT('Ctrl Pts',(-9.38336846546382,-0.567928885365873,
14.9113882007562));
#28972=CARTESIAN_POINT('Ctrl Pts',(-9.4751422111953,-0.425182052581577,
14.9036702271398));
#28973=CARTESIAN_POINT('Ctrl Pts',(-9.53160998347358,-0.259736422802674,
14.8959522535235));
#28974=CARTESIAN_POINT('Ctrl Pts',(-9.54626123844843,-0.0906670911680779,
14.8882342799071));
#28975=CARTESIAN_POINT('Ctrl Pts',(-9.54887290460746,-0.0605295601021361,
14.8868585089889));
#28976=CARTESIAN_POINT('Ctrl Pts',(-9.55015585058872,-0.0302768858802269,
14.8854827380706));
#28977=CARTESIAN_POINT('Ctrl Pts',(-9.55012781659967,-2.18430157070126E-5,
14.8841069671524));
#28978=CARTESIAN_POINT('Origin',(-8.5,0.,13.7));
#28979=CARTESIAN_POINT('',(-9.55014776911894,-1.85392180561128E-5,14.5841069671524));
#28980=CARTESIAN_POINT('',(-9.55002842899351,-9.63116671427123E-6,14.6658930328476));
#28981=CARTESIAN_POINT('',(-9.5501,-1.28600160378464E-16,13.7));
#28982=CARTESIAN_POINT('Ctrl Pts',(-9.55002842899351,-9.63116671427123E-6,
14.6658930328476));
#28983=CARTESIAN_POINT('Ctrl Pts',(-9.55005326673695,-0.0729826631512053,
14.6692103912693));
#28984=CARTESIAN_POINT('Ctrl Pts',(-9.54254596316782,-0.145950655912037,
14.6725277496911));
#28985=CARTESIAN_POINT('Ctrl Pts',(-9.52745206094249,-0.217314024833131,
14.6758451081128));
#28986=CARTESIAN_POINT('Ctrl Pts',(-9.49233546383911,-0.383343898150939,
14.6835630817291));
#28987=CARTESIAN_POINT('Ctrl Pts',(-9.41615414400742,-0.540688267457234,
14.6912810553455));
#28988=CARTESIAN_POINT('Ctrl Pts',(-9.30769139353042,-0.671206180295421,
14.6989990289619));
#28989=CARTESIAN_POINT('Ctrl Pts',(-9.19922864305341,-0.801724093133606,
14.7067170025782));
#28990=CARTESIAN_POINT('Ctrl Pts',(-9.05848446193109,-0.905415549503684,
14.7144349761946));
#28991=CARTESIAN_POINT('Ctrl Pts',(-8.90168588647599,-0.970325496300035,
14.722152949811));
#28992=CARTESIAN_POINT('Ctrl Pts',(-8.74488731102089,-1.03523544309639,
14.7298709234273));
#28993=CARTESIAN_POINT('Ctrl Pts',(-8.57203434123302,-1.06136388031901,
14.7375888970437));
#28994=CARTESIAN_POINT('Ctrl Pts',(-8.40305598661677,-1.04569832567051,
14.74530687066));
#28995=CARTESIAN_POINT('Ctrl Pts',(-8.23407763200053,-1.03003277102201,
14.7530248442764));
#28996=CARTESIAN_POINT('Ctrl Pts',(-8.06897389255591,-0.972573224502382,
14.7607428178928));
#28997=CARTESIAN_POINT('Ctrl Pts',(-7.92678032355634,-0.879944493087918,
14.7684607915091));
#28998=CARTESIAN_POINT('Ctrl Pts',(-7.78458675455677,-0.787315761673454,
14.7761787651255));
#28999=CARTESIAN_POINT('Ctrl Pts',(-7.66530335600225,-0.659517845364154,
14.7838967387419));
#29000=CARTESIAN_POINT('Ctrl Pts',(-7.5826828692813,-0.511285074047506,
14.7916147123582));
#29001=CARTESIAN_POINT('Ctrl Pts',(-7.50006238256035,-0.363052302730855,
14.7993326859746));
#29002=CARTESIAN_POINT('Ctrl Pts',(-7.45410480767297,-0.194384676406854,
14.8070506595909));
#29003=CARTESIAN_POINT('Ctrl Pts',(-7.45010876983605,-0.0247288141878713,
14.8147686332073));
#29004=CARTESIAN_POINT('Ctrl Pts',(-7.44611273199913,0.144927048031107,
14.8224866068237));
#29005=CARTESIAN_POINT('Ctrl Pts',(-7.48407823121267,0.315571146145067,
14.83020458044));
#29006=CARTESIAN_POINT('Ctrl Pts',(-7.5596281217401,0.467529493626993,14.8379225540564));
#29007=CARTESIAN_POINT('Ctrl Pts',(-7.63517801226754,0.619487841108922,
14.8456405276727));
#29008=CARTESIAN_POINT('Ctrl Pts',(-7.74831229410887,0.752760437958817,
14.8533585012891));
#29009=CARTESIAN_POINT('Ctrl Pts',(-7.88598704248203,0.851980929732758,
14.8610764749055));
#29010=CARTESIAN_POINT('Ctrl Pts',(-8.02366179085519,0.951201421506699,
14.8687944485218));
#29011=CARTESIAN_POINT('Ctrl Pts',(-8.18587700576016,1.01636980820469,14.8765124221382));
#29012=CARTESIAN_POINT('Ctrl Pts',(-8.35393047093769,1.03997418164186,14.8842303957546));
#29013=CARTESIAN_POINT('Ctrl Pts',(-8.52198393611523,1.06357855507904,14.8919483693709));
#29014=CARTESIAN_POINT('Ctrl Pts',(-8.69587565156532,1.0456189152554,14.8996663429873));
#29015=CARTESIAN_POINT('Ctrl Pts',(-8.85555605774434,0.988162433411327,
14.9073843166036));
#29016=CARTESIAN_POINT('Ctrl Pts',(-9.01523646392337,0.930705951567249,
14.91510229022));
#29017=CARTESIAN_POINT('Ctrl Pts',(-9.16070556083133,0.833752627702728,
14.9228202638364));
#29018=CARTESIAN_POINT('Ctrl Pts',(-9.27519284226569,0.708488603778973,
14.9305382374527));
#29019=CARTESIAN_POINT('Ctrl Pts',(-9.38968012370006,0.583224579855222,
14.9382562110691));
#29020=CARTESIAN_POINT('Ctrl Pts',(-9.47318558966083,0.429649855872239,
14.9459741846855));
#29021=CARTESIAN_POINT('Ctrl Pts',(-9.516077074097,0.265455038662242,14.9536921583018));
#29022=CARTESIAN_POINT('Ctrl Pts',(-9.53867858613031,0.178933175738607,
14.9577591164838));
#29023=CARTESIAN_POINT('Ctrl Pts',(-9.55000271331294,0.0894624052226828,
14.9618260746657));
#29024=CARTESIAN_POINT('Ctrl Pts',(-9.55001141291652,-2.01662567329067E-6,
14.9658930328476));
#29025=CARTESIAN_POINT('Ctrl Pts',(-9.55012781659967,-2.18430157070126E-5,
14.8841069671524));
#29026=CARTESIAN_POINT('Ctrl Pts',(-9.54999858197299,0.139451678297384,
14.8777647644543));
#29027=CARTESIAN_POINT('Ctrl Pts',(-9.52200915934138,0.278975536633117,
14.8714225617561));
#29028=CARTESIAN_POINT('Ctrl Pts',(-9.46789751229482,0.407501496024797,
14.865080359058));
#29029=CARTESIAN_POINT('Ctrl Pts',(-9.40204779349493,0.563907718092787,
14.8573623854417));
#29030=CARTESIAN_POINT('Ctrl Pts',(-9.29751361822373,0.704027128738476,
14.8496444118253));
#29031=CARTESIAN_POINT('Ctrl Pts',(-9.16634718282251,0.811704698310384,
14.8419264382089));
#29032=CARTESIAN_POINT('Ctrl Pts',(-9.0351807474213,0.919382267882293,14.8342084645926));
#29033=CARTESIAN_POINT('Ctrl Pts',(-8.87738205189007,0.994617996380422,
14.8264904909762));
#29034=CARTESIAN_POINT('Ctrl Pts',(-8.71114443817192,1.02873762525396,14.8187725173598));
#29035=CARTESIAN_POINT('Ctrl Pts',(-8.54490682445378,1.0628572541275,14.8110545437435));
#29036=CARTESIAN_POINT('Ctrl Pts',(-8.37023029254873,1.05586078337645,14.8033365701271));
#29037=CARTESIAN_POINT('Ctrl Pts',(-8.20725409024193,1.00855486276817,14.7956185965108));
#29038=CARTESIAN_POINT('Ctrl Pts',(-8.04427788793513,0.961248942159876,
14.7879006228944));
#29039=CARTESIAN_POINT('Ctrl Pts',(-7.89300201522659,0.873633571694345,
14.780182649278));
#29040=CARTESIAN_POINT('Ctrl Pts',(-7.77086775905398,0.755810328966214,
14.7724646756617));
#29041=CARTESIAN_POINT('Ctrl Pts',(-7.64873350288136,0.637987086238083,
14.7647467020453));
#29042=CARTESIAN_POINT('Ctrl Pts',(-7.55574086324466,0.489955971247353,
14.7570287284289));
#29043=CARTESIAN_POINT('Ctrl Pts',(-7.50261138405976,0.328784164475392,
14.7493107548126));
#29044=CARTESIAN_POINT('Ctrl Pts',(-7.44948190487485,0.167612357703432,
14.7415927811962));
#29045=CARTESIAN_POINT('Ctrl Pts',(-7.43621558614173,-0.00670014084975726,
14.7338748075799));
#29046=CARTESIAN_POINT('Ctrl Pts',(-7.46434196270175,-0.174056048645625,
14.7261568339635));
#29047=CARTESIAN_POINT('Ctrl Pts',(-7.49246833926176,-0.341411956441492,
14.7184388603471));
#29048=CARTESIAN_POINT('Ctrl Pts',(-7.56198741111491,-0.501811273480041,
14.7107208867308));
#29049=CARTESIAN_POINT('Ctrl Pts',(-7.6648840075379,-0.636760832049021,
14.7030029131144));
#29050=CARTESIAN_POINT('Ctrl Pts',(-7.76778060396089,-0.771710390618001,
14.695284939498));
#29051=CARTESIAN_POINT('Ctrl Pts',(-7.90405472495371,-0.881210190717416,
14.6875669658817));
#29052=CARTESIAN_POINT('Ctrl Pts',(-8.05799470643122,-0.952635501466403,
14.6798489922653));
#29053=CARTESIAN_POINT('Ctrl Pts',(-8.21193468790874,-1.02406081221539,
14.672131018649));
#29054=CARTESIAN_POINT('Ctrl Pts',(-8.38354052987094,-1.05741163361395,
14.6644130450326));
#29055=CARTESIAN_POINT('Ctrl Pts',(-8.55302701300903,-1.04884279758615,
14.6566950714162));
#29056=CARTESIAN_POINT('Ctrl Pts',(-8.72251349614711,-1.04027396155835,
14.6489770977999));
#29057=CARTESIAN_POINT('Ctrl Pts',(-8.88988062046108,-0.989785468104193,
14.6412591241835));
#29058=CARTESIAN_POINT('Ctrl Pts',(-9.03583186778373,-0.903198365607414,
14.6335411505671));
#29059=CARTESIAN_POINT('Ctrl Pts',(-9.18178311510637,-0.816611263110635,
14.6258231769508));
#29060=CARTESIAN_POINT('Ctrl Pts',(-9.30631848543768,-0.693925551571234,
14.6181052033344));
#29061=CARTESIAN_POINT('Ctrl Pts',(-9.39507972860953,-0.549286225569062,
14.6103872297181));
#29062=CARTESIAN_POINT('Ctrl Pts',(-9.48384097178138,-0.404646899566892,
14.6026692561017));
#29063=CARTESIAN_POINT('Ctrl Pts',(-9.53682808779378,-0.238053959101951,
14.5949512824853));
#29064=CARTESIAN_POINT('Ctrl Pts',(-9.54793195066775,-0.0687146631774201,
14.587233308869));
#29065=CARTESIAN_POINT('Ctrl Pts',(-9.54943124186531,-0.0458497450256745,
14.5861911949634));
#29066=CARTESIAN_POINT('Ctrl Pts',(-9.55016693607009,-0.0229347565328515,
14.5851490810579));
#29067=CARTESIAN_POINT('Ctrl Pts',(-9.55014776911894,-1.85392180561128E-5,
14.5841069671524));
#29068=CARTESIAN_POINT('Origin',(-8.5,0.,13.7));
#29069=CARTESIAN_POINT('',(-9.55016480120948,-1.36965928395627E-5,14.2841069671524));
#29070=CARTESIAN_POINT('',(-9.55003832846065,-1.48519270705213E-5,14.3658930328476));
#29071=CARTESIAN_POINT('',(-9.5501,-1.28600160378464E-16,13.7));
#29072=CARTESIAN_POINT('Ctrl Pts',(-9.55003832846065,-1.48519270705213E-5,
14.3658930328476));
#29073=CARTESIAN_POINT('Ctrl Pts',(-9.550073241473,-0.0656465445328537,
14.3688767342566));
#29074=CARTESIAN_POINT('Ctrl Pts',(-9.54400906450974,-0.131271863811158,
14.3718604356656));
#29075=CARTESIAN_POINT('Ctrl Pts',(-9.5317817860297,-0.19572804844434,14.3748441370746));
#29076=CARTESIAN_POINT('Ctrl Pts',(-9.50015334880606,-0.36245757805093,
14.382562110691));
#29077=CARTESIAN_POINT('Ctrl Pts',(-9.42728714065459,-0.521364340736037,
14.3902800843074));
#29078=CARTESIAN_POINT('Ctrl Pts',(-9.3215842386497,-0.654127251941727,
14.3979980579237));
#29079=CARTESIAN_POINT('Ctrl Pts',(-9.21588133664482,-0.786890163147415,
14.4057160315401));
#29080=CARTESIAN_POINT('Ctrl Pts',(-9.07734174078653,-0.893509222873686,
14.4134340051565));
#29081=CARTESIAN_POINT('Ctrl Pts',(-8.92193831218837,-0.961691834029087,
14.4211519787728));
#29082=CARTESIAN_POINT('Ctrl Pts',(-8.7665348835902,-1.02987444518449,14.4288699523892));
#29083=CARTESIAN_POINT('Ctrl Pts',(-8.59426762225216,-1.05962060776902,
14.4365879260055));
#29084=CARTESIAN_POINT('Ctrl Pts',(-8.42499800548463,-1.04750075119252,
14.4443058996219));
#29085=CARTESIAN_POINT('Ctrl Pts',(-8.25572838871711,-1.03538089461602,
14.4520238732383));
#29086=CARTESIAN_POINT('Ctrl Pts',(-8.08945641652011,-0.981395018878487,
14.4597418468546));
#29087=CARTESIAN_POINT('Ctrl Pts',(-7.94535234200829,-0.891767401520943,
14.467459820471));
#29088=CARTESIAN_POINT('Ctrl Pts',(-7.80124826749647,-0.802139784163398,
14.4751777940874));
#29089=CARTESIAN_POINT('Ctrl Pts',(-7.67931209066984,-0.676870425185841,
14.4828957677037));
#29090=CARTESIAN_POINT('Ctrl Pts',(-7.59360238882539,-0.530402199643331,
14.4906137413201));
#29091=CARTESIAN_POINT('Ctrl Pts',(-7.50789268698095,-0.383933974100822,
14.4983317149364));
#29092=CARTESIAN_POINT('Ctrl Pts',(-7.4584094601187,-0.216266881993361,
14.5060496885528));
#29093=CARTESIAN_POINT('Ctrl Pts',(-7.4508578548822,-0.0467320261582989,
14.5137676621692));
#29094=CARTESIAN_POINT('Ctrl Pts',(-7.44330624964569,0.122802829676763,
14.5214856357855));
#29095=CARTESIAN_POINT('Ctrl Pts',(-7.47768626603494,0.294205449239426,
14.5292036094019));
#29096=CARTESIAN_POINT('Ctrl Pts',(-7.55003407534174,0.447714043693381,
14.5369215830183));
#29097=CARTESIAN_POINT('Ctrl Pts',(-7.62238188464855,0.601222638147337,
14.5446395566346));
#29098=CARTESIAN_POINT('Ctrl Pts',(-7.73269748687292,0.736837207492585,
14.552357530251));
#29099=CARTESIAN_POINT('Ctrl Pts',(-7.86826209370633,0.838922130279325,
14.5600755038673));
#29100=CARTESIAN_POINT('Ctrl Pts',(-8.00382670053974,0.941007053066066,
14.5677934774837));
#29101=CARTESIAN_POINT('Ctrl Pts',(-8.16464031198218,1.0095623292943,14.5755114511001));
#29102=CARTESIAN_POINT('Ctrl Pts',(-8.33216199418164,1.03668390879925,14.5832294247164));
#29103=CARTESIAN_POINT('Ctrl Pts',(-8.4996836763811,1.06380548830419,14.5909473983328));
#29104=CARTESIAN_POINT('Ctrl Pts',(-8.67391342933756,1.04949337108586,14.5986653719492));
#29105=CARTESIAN_POINT('Ctrl Pts',(-8.83476351117266,0.995397666487676,
14.6063833455655));
#29106=CARTESIAN_POINT('Ctrl Pts',(-8.99561359300775,0.941301961889491,
14.6141013191819));
#29107=CARTESIAN_POINT('Ctrl Pts',(-9.14308400372149,0.847422669911453,
14.6218192927982));
#29108=CARTESIAN_POINT('Ctrl Pts',(-9.26017220780516,0.724583561457418,
14.6295372664146));
#29109=CARTESIAN_POINT('Ctrl Pts',(-9.37726041188882,0.601744453003383,
14.637255240031));
#29110=CARTESIAN_POINT('Ctrl Pts',(-9.46396640934243,0.44994552807335,14.6449732136473));
#29111=CARTESIAN_POINT('Ctrl Pts',(-9.51029347088169,0.286688376943674,
14.6526911872637));
#29112=CARTESIAN_POINT('Ctrl Pts',(-9.53670812077122,0.193602816457645,
14.6570918024583));
#29113=CARTESIAN_POINT('Ctrl Pts',(-9.54999548068424,0.0967921588502287,
14.661492417653));
#29114=CARTESIAN_POINT('Ctrl Pts',(-9.55002842899351,-9.63116671427123E-6,
14.6658930328476));
#29115=CARTESIAN_POINT('Ctrl Pts',(-9.55014776911894,-1.85392180561128E-5,
14.5841069671524));
#29116=CARTESIAN_POINT('Ctrl Pts',(-9.55002498419467,0.146784464834437,
14.5774311074415));
#29117=CARTESIAN_POINT('Ctrl Pts',(-9.51892436163577,0.293637897031557,
14.5707552477307));
#29118=CARTESIAN_POINT('Ctrl Pts',(-9.4591424759889,0.427701752301033,14.5640793880199));
#29119=CARTESIAN_POINT('Ctrl Pts',(-9.39002852870054,0.582693220470828,
14.5563614144035));
#29120=CARTESIAN_POINT('Ctrl Pts',(-9.28258002438829,0.720590505426293,
14.5486434407872));
#29121=CARTESIAN_POINT('Ctrl Pts',(-9.14918519058914,0.825494801005002,
14.5409254671708));
#29122=CARTESIAN_POINT('Ctrl Pts',(-9.01579035679,0.930399096583712,14.5332074935544));
#29123=CARTESIAN_POINT('Ctrl Pts',(-8.85644919350396,1.00231040278566,14.5254895199381));
#29124=CARTESIAN_POINT('Ctrl Pts',(-8.68953286931277,1.03293773753167,14.5177715463217));
#29125=CARTESIAN_POINT('Ctrl Pts',(-8.52261654512158,1.06356507227767,14.5100535727053));
#29126=CARTESIAN_POINT('Ctrl Pts',(-8.34812506002524,1.05290843556774,14.502335599089));
#29127=CARTESIAN_POINT('Ctrl Pts',(-8.18617633222389,1.00219647959389,14.4946176254726));
#29128=CARTESIAN_POINT('Ctrl Pts',(-8.02422760442253,0.951484523620035,
14.4868996518563));
#29129=CARTESIAN_POINT('Ctrl Pts',(-7.87482163391617,0.860717248382274,
14.4791816782399));
#29130=CARTESIAN_POINT('Ctrl Pts',(-7.75518411565231,0.740359626526339,
14.4714637046235));
#29131=CARTESIAN_POINT('Ctrl Pts',(-7.63554659738845,0.620002004670402,
14.4637457310072));
#29132=CARTESIAN_POINT('Ctrl Pts',(-7.54567753136709,0.470054036196291,
14.4560277573908));
#29133=CARTESIAN_POINT('Ctrl Pts',(-7.49593833160183,0.307803905466374,
14.4483097837744));
#29134=CARTESIAN_POINT('Ctrl Pts',(-7.44619913183657,0.145553774736457,
14.4405918101581));
#29135=CARTESIAN_POINT('Ctrl Pts',(-7.4365897983274,-0.0289985182492672,
14.4328738365417));
#29136=CARTESIAN_POINT('Ctrl Pts',(-7.46821823490919,-0.195728044472262,
14.4251558629254));
#29137=CARTESIAN_POINT('Ctrl Pts',(-7.49984667149097,-0.362457570695256,
14.417437889309));
#29138=CARTESIAN_POINT('Ctrl Pts',(-7.5727128781637,-0.521364330155521,
14.4097199156926));
#29139=CARTESIAN_POINT('Ctrl Pts',(-7.67841577802345,-0.654127238666931,
14.4020019420763));
#29140=CARTESIAN_POINT('Ctrl Pts',(-7.78411867788321,-0.786890147178342,
14.3942839684599));
#29141=CARTESIAN_POINT('Ctrl Pts',(-7.92265827092999,-0.893509204740896,
14.3865659948435));
#29142=CARTESIAN_POINT('Ctrl Pts',(-8.07806169637442,-0.961691814512604,
14.3788480212272));
#29143=CARTESIAN_POINT('Ctrl Pts',(-8.23346512181885,-1.02987442428431,
14.3711300476108));
#29144=CARTESIAN_POINT('Ctrl Pts',(-8.40573237966092,-1.05962058626517,
14.3634120739945));
#29145=CARTESIAN_POINT('Ctrl Pts',(-8.5750019929933,-1.04750072993463,14.3556941003781));
#29146=CARTESIAN_POINT('Ctrl Pts',(-8.74427160632568,-1.03538087360409,
14.3479761267617));
#29147=CARTESIAN_POINT('Ctrl Pts',(-8.91054357514837,-0.981394998962145,
14.3402581531454));
#29148=CARTESIAN_POINT('Ctrl Pts',(-9.05464764673576,-0.89176738342349,
14.332540179529));
#29149=CARTESIAN_POINT('Ctrl Pts',(-9.19875171832314,-0.802139767884835,
14.3248222059126));
#29150=CARTESIAN_POINT('Ctrl Pts',(-9.32068789267521,-0.676870411449469,
14.3171042322963));
#29151=CARTESIAN_POINT('Ctrl Pts',(-9.40639759278026,-0.530402188879377,
14.3093862586799));
#29152=CARTESIAN_POINT('Ctrl Pts',(-9.49210729288531,-0.383933966309286,
14.3016682850636));
#29153=CARTESIAN_POINT('Ctrl Pts',(-9.54159051874335,-0.216266877604468,
14.2939503114472));
#29154=CARTESIAN_POINT('Ctrl Pts',(-9.5491421238266,-0.0467320252099184,
14.2862323378308));
#29155=CARTESIAN_POINT('Ctrl Pts',(-9.54983530923238,-0.0311698918414938,
14.285523880938));
#29156=CARTESIAN_POINT('Ctrl Pts',(-9.55017517975655,-0.0155920207387595,
14.2848154240452));
#29157=CARTESIAN_POINT('Ctrl Pts',(-9.55016480120948,-1.36965928395627E-5,
14.2841069671524));
#29158=CARTESIAN_POINT('Origin',(-8.5,0.,13.7));
#29159=CARTESIAN_POINT('',(-9.55017700723911,-7.61513114500012E-6,13.9841069671524));
#29160=CARTESIAN_POINT('',(-9.5500522825869,-1.91003407042144E-5,14.0658930328476));
#29161=CARTESIAN_POINT('',(-9.5501,-1.28600160378464E-16,13.7));
#29162=CARTESIAN_POINT('',(-7.70661869325991,-0.687936125025711,13.8));
#29163=CARTESIAN_POINT('Ctrl Pts',(-9.55017700723911,-7.61513114500012E-6,
13.9841069671524));
#29164=CARTESIAN_POINT('Ctrl Pts',(-9.55011125498444,0.161456600375193,
13.9767637934161));
#29165=CARTESIAN_POINT('Ctrl Pts',(-9.51225289750323,0.322950533171347,
13.9694206196799));
#29166=CARTESIAN_POINT('Ctrl Pts',(-9.44037185879917,0.467529483605666,
13.9620774459436));
#29167=CARTESIAN_POINT('Ctrl Pts',(-9.36482196986006,0.61948782818686,13.9543594723273));
#29168=CARTESIAN_POINT('Ctrl Pts',(-9.25168769073042,0.752760423312007,
13.9466414987109));
#29169=CARTESIAN_POINT('Ctrl Pts',(-9.11401294444701,0.851980912188383,
13.9389235250945));
#29170=CARTESIAN_POINT('Ctrl Pts',(-8.97633819816361,0.95120140106476,13.9312055514782));
#29171=CARTESIAN_POINT('Ctrl Pts',(-8.81412298472643,1.01636978369236,13.9234875778618));
#29172=CARTESIAN_POINT('Ctrl Pts',(-8.64606952266772,1.03997415669788,13.9157696042454));
#29173=CARTESIAN_POINT('Ctrl Pts',(-8.478016060609,1.0635785297034,13.9080516306291));
#29174=CARTESIAN_POINT('Ctrl Pts',(-8.30412434992875,1.04561889308684,13.9003336570127));
#29175=CARTESIAN_POINT('Ctrl Pts',(-8.14444394193064,0.988162407251559,
13.8926156833964));
#29176=CARTESIAN_POINT('Ctrl Pts',(-7.98476353393253,0.930705921416282,
13.88489770978));
#29177=CARTESIAN_POINT('Ctrl Pts',(-7.83929442861656,0.833752586362294,
13.8771797361636));
#29178=CARTESIAN_POINT('Ctrl Pts',(-7.72480714475875,0.708488560736079,
13.8694617625473));
#29179=CARTESIAN_POINT('Ctrl Pts',(-7.61031986090093,0.583224535109864,
13.8617437889309));
#29180=CARTESIAN_POINT('Ctrl Pts',(-7.52681439850127,0.429649818911422,
13.8540258153145));
#29181=CARTESIAN_POINT('Ctrl Pts',(-7.48392288713058,0.265454980301966,
13.8463078416982));
#29182=CARTESIAN_POINT('Ctrl Pts',(-7.44103137575989,0.101260141692509,
13.8385898680818));
#29183=CARTESIAN_POINT('Ctrl Pts',(-7.43875381541816,-0.0735548193279625,
13.8308718944655));
#29184=CARTESIAN_POINT('Ctrl Pts',(-7.47735030989339,-0.238792383161204,
13.8231539208491));
#29185=CARTESIAN_POINT('Ctrl Pts',(-7.51594680436863,-0.404029946994446,
13.8154359472327));
#29186=CARTESIAN_POINT('Ctrl Pts',(-7.59541735366082,-0.559690113640457,
13.8077179736164));
#29187=CARTESIAN_POINT('Ctrl Pts',(-7.70661869325992,-0.687936125025717,
13.8));
#29188=CARTESIAN_POINT('',(-9.29341905289386,-0.68794083902029,13.8));
#29189=CARTESIAN_POINT('Origin',(-8.5,0.,13.8));
#29190=CARTESIAN_POINT('Ctrl Pts',(-9.29341905289386,-0.68794083902029,
13.8));
#29191=CARTESIAN_POINT('Ctrl Pts',(-9.20135839317727,-0.793915425263775,
13.8063833455655));
#29192=CARTESIAN_POINT('Ctrl Pts',(-9.08793164264836,-0.881430588389637,
13.812766691131));
#29193=CARTESIAN_POINT('Ctrl Pts',(-8.96187776001814,-0.943160400251609,
13.8191500366965));
#29194=CARTESIAN_POINT('Ctrl Pts',(-8.80946856794249,-1.01779666338413,
13.8268680103129));
#29195=CARTESIAN_POINT('Ctrl Pts',(-8.63860010291811,-1.05473799838573,
13.8345859839293));
#29196=CARTESIAN_POINT('Ctrl Pts',(-8.4689713820678,-1.04972407874521,13.8423039575456));
#29197=CARTESIAN_POINT('Ctrl Pts',(-8.29934266121749,-1.04471015910468,
13.850021931162));
#29198=CARTESIAN_POINT('Ctrl Pts',(-8.13095368454124,-0.997740984822029,
13.8577399047784));
#29199=CARTESIAN_POINT('Ctrl Pts',(-7.98321933527585,-0.914232378227999,
13.8654578783947));
#29200=CARTESIAN_POINT('Ctrl Pts',(-7.83548498601045,-0.830723771633969,
13.8731758520111));
#29201=CARTESIAN_POINT('Ctrl Pts',(-7.70840526415591,-0.710675732728563,
13.8808938256275));
#29202=CARTESIAN_POINT('Ctrl Pts',(-7.61663151655039,-0.567928896847351,
13.8886117992438));
#29203=CARTESIAN_POINT('Ctrl Pts',(-7.52485776894487,-0.425182060966139,
13.8963297728602));
#29204=CARTESIAN_POINT('Ctrl Pts',(-7.46838999558837,-0.259736428109122,
13.9040477464765));
#29205=CARTESIAN_POINT('Ctrl Pts',(-7.45373874033249,-0.0906670931082204,
13.9117657200929));
#29206=CARTESIAN_POINT('Ctrl Pts',(-7.43908748507661,0.0784022418926819,
13.9194836937093));
#29207=CARTESIAN_POINT('Ctrl Pts',(-7.46625274792135,0.251095279037468,
13.9272016673256));
#29208=CARTESIAN_POINT('Ctrl Pts',(-7.53210246805017,0.407501504320363,
13.934919640942));
#29209=CARTESIAN_POINT('Ctrl Pts',(-7.59795218817899,0.563907729603256,
13.9426376145584));
#29210=CARTESIAN_POINT('Ctrl Pts',(-7.7024863655919,0.704027143024259,13.9503555881747));
#29211=CARTESIAN_POINT('Ctrl Pts',(-7.83365280365984,0.811704714764279,
13.9580735617911));
#29212=CARTESIAN_POINT('Ctrl Pts',(-7.96481924172778,0.919382286504301,
13.9657915354074));
#29213=CARTESIAN_POINT('Ctrl Pts',(-8.12261794045076,0.99461801656334,13.9735095090238));
#29214=CARTESIAN_POINT('Ctrl Pts',(-8.28885555754004,1.02873764613831,13.9812274826402));
#29215=CARTESIAN_POINT('Ctrl Pts',(-8.45509317462931,1.06285727571327,13.9889454562565));
#29216=CARTESIAN_POINT('Ctrl Pts',(-8.62976971008488,1.05586080480417,13.9966634298729));
#29217=CARTESIAN_POINT('Ctrl Pts',(-8.79274591570048,1.00855488323173,14.0043814034893));
#29218=CARTESIAN_POINT('Ctrl Pts',(-8.95572212131607,0.961248961659288,
14.0120993771056));
#29219=CARTESIAN_POINT('Ctrl Pts',(-9.10699799709169,0.873633589423514,
14.019817350722));
#29220=CARTESIAN_POINT('Ctrl Pts',(-9.22913225574218,0.755810344306336,
14.0275353243383));
#29221=CARTESIAN_POINT('Ctrl Pts',(-9.35126651439268,0.637987099189158,
14.0352532979547));
#29222=CARTESIAN_POINT('Ctrl Pts',(-9.44425915591805,0.489955981190576,
14.0429712715711));
#29223=CARTESIAN_POINT('Ctrl Pts',(-9.49738863618153,0.328784171146844,
14.0506892451874));
#29224=CARTESIAN_POINT('Ctrl Pts',(-9.53227557138735,0.222952334168298,
14.0557571744075));
#29225=CARTESIAN_POINT('Ctrl Pts',(-9.54997447121724,0.111454547160044,
14.0608251036276));
#29226=CARTESIAN_POINT('Ctrl Pts',(-9.5500522825869,-1.91003407042144E-5,
14.0658930328476));
#29227=CARTESIAN_POINT('Origin',(-8.5,0.,13.1374873996035));
#29228=CARTESIAN_POINT('',(-9.71736702302461,-1.11660450847761E-5,14.7625126003965));
#29229=CARTESIAN_POINT('',(-9.71748224961362,-2.53240448353063E-5,14.7874873996035));
#29230=CARTESIAN_POINT('',(-9.71745,1.55202226700376E-15,13.1374873996035));
#29231=CARTESIAN_POINT('',(-8.18521110449559,1.17604951161383,15.));
#29232=CARTESIAN_POINT('Ctrl Pts',(-9.71748224961362,-2.53240448353162E-5,
14.7874873996035));
#29233=CARTESIAN_POINT('Ctrl Pts',(-9.71751475126106,-0.035101985253679,
14.7888631705217));
#29234=CARTESIAN_POINT('Ctrl Pts',(-9.70768312250827,-0.266937983084884,
14.7979569150563));
#29235=CARTESIAN_POINT('Ctrl Pts',(-9.56507970256121,-0.68475352051211,
14.8147686332073));
#29236=CARTESIAN_POINT('Ctrl Pts',(-9.12308407132213,-1.10229227255141,
14.8379225540564));
#29237=CARTESIAN_POINT('Ctrl Pts',(-8.53741083331568,-1.26565563225515,
14.8610764749055));
#29238=CARTESIAN_POINT('Ctrl Pts',(-7.94311369450983,-1.13717006497505,
14.8842303957546));
#29239=CARTESIAN_POINT('Ctrl Pts',(-7.47722284672394,-0.74647126776861,
14.9073843166036));
#29240=CARTESIAN_POINT('Ctrl Pts',(-7.24718575990748,-0.183633090657203,
14.9305382374527));
#29241=CARTESIAN_POINT('Ctrl Pts',(-7.3060080642777,0.421519192034503,14.9536921583018));
#29242=CARTESIAN_POINT('Ctrl Pts',(-7.64021279447249,0.92951767940246,14.9768460791509));
#29243=CARTESIAN_POINT('Ctrl Pts',(-7.99510874416173,1.12516550422186,14.9922820263836));
#29244=CARTESIAN_POINT('Ctrl Pts',(-8.18521110449559,1.17604951161383,15.));
#29245=CARTESIAN_POINT('',(-8.81478889550434,1.17604951161384,15.));
#29246=CARTESIAN_POINT('Origin',(-8.5,0.,15.));
#29247=CARTESIAN_POINT('Ctrl Pts',(-9.71736702302461,-1.11660450847831E-5,
14.7625126003965));
#29248=CARTESIAN_POINT('Ctrl Pts',(-9.71739581905428,-0.0846136018031169,
14.7658299588182));
#29249=CARTESIAN_POINT('Ctrl Pts',(-9.68844255967355,-0.366027720925746,
14.7768652908563));
#29250=CARTESIAN_POINT('Ctrl Pts',(-9.47383574401748,-0.809275148678942,
14.7956185965108));
#29251=CARTESIAN_POINT('Ctrl Pts',(-8.98431378427829,-1.16992412560805,
14.8187725173598));
#29252=CARTESIAN_POINT('Ctrl Pts',(-8.38311433260251,-1.26080137319404,
14.8419264382089));
#29253=CARTESIAN_POINT('Ctrl Pts',(-7.80886745824715,-1.06095147820218,
14.865080359058));
#29254=CARTESIAN_POINT('Ctrl Pts',(-7.39398818892938,-0.616457887465797,
14.8882342799071));
#29255=CARTESIAN_POINT('Ctrl Pts',(-7.23414327069309,-0.0298154676920097,
14.9113882007562));
#29256=CARTESIAN_POINT('Ctrl Pts',(-7.36619097191447,0.563701313325544,
14.9345421216053));
#29257=CARTESIAN_POINT('Ctrl Pts',(-7.75968301484676,1.02723637580027,14.9576960424544));
#29258=CARTESIAN_POINT('Ctrl Pts',(-8.29136193563724,1.24083321706785,14.9795153352526));
#29259=CARTESIAN_POINT('Ctrl Pts',(-8.6575692829609,1.2180150268885,14.9936166544345));
#29260=CARTESIAN_POINT('Ctrl Pts',(-8.81482207543406,1.17607856395779,15.));
#29261=CARTESIAN_POINT('Origin',(-8.5,0.,13.1374873996035));
#29262=CARTESIAN_POINT('',(-9.717378500128,-1.72188158990005E-5,14.4625126003965));
#29263=CARTESIAN_POINT('',(-9.71750538188158,-2.1493734860395E-5,14.4874873996035));
#29264=CARTESIAN_POINT('',(-9.71745,1.55202226700376E-15,13.1374873996035));
#29265=CARTESIAN_POINT('Ctrl Pts',(-9.71750538188158,-2.14937348604928E-5,
14.4874873996035));
#29266=CARTESIAN_POINT('Ctrl Pts',(-9.71752760338875,-0.0265897717749626,
14.488529513509));
#29267=CARTESIAN_POINT('Ctrl Pts',(-9.71035773696392,-0.249912730625655,
14.4972896010309));
#29268=CARTESIAN_POINT('Ctrl Pts',(-9.57920010161505,-0.662275919671228,
14.5137676621692));
#29269=CARTESIAN_POINT('Ctrl Pts',(-9.14605396331434,-1.08898876467735,
14.5369215830183));
#29270=CARTESIAN_POINT('Ctrl Pts',(-8.56393481610157,-1.2645926586563,14.5600755038673));
#29271=CARTESIAN_POINT('Ctrl Pts',(-7.96707299637902,-1.14859525599462,
14.5832294247164));
#29272=CARTESIAN_POINT('Ctrl Pts',(-7.49309834081465,-0.767744294283258,
14.6063833455655));
#29273=CARTESIAN_POINT('Ctrl Pts',(-7.25130424303077,-0.209859858909738,
14.6295372664146));
#29274=CARTESIAN_POINT('Ctrl Pts',(-7.29744579071662,0.396415975859085,
14.6526911872637));
#29275=CARTESIAN_POINT('Ctrl Pts',(-7.62088324179469,0.911282600786611,
14.6758451081128));
#29276=CARTESIAN_POINT('Ctrl Pts',(-8.14703544985776,1.21601738634968,14.6989990289619));
#29277=CARTESIAN_POINT('Ctrl Pts',(-8.75457742805358,1.2403517925468,14.722152949811));
#29278=CARTESIAN_POINT('Ctrl Pts',(-9.3034166487216,0.978674606583422,14.74530687066));
#29279=CARTESIAN_POINT('Ctrl Pts',(-9.6453933088254,0.520283195889185,14.7670850205909));
#29280=CARTESIAN_POINT('Ctrl Pts',(-9.71733241941055,0.1616755030408,14.7811451969054));
#29281=CARTESIAN_POINT('Ctrl Pts',(-9.71748224961362,-2.53240448353162E-5,
14.7874873996035));
#29282=CARTESIAN_POINT('Ctrl Pts',(-9.717378500128,-1.72188158990352E-5,
14.4625126003965));
#29283=CARTESIAN_POINT('Ctrl Pts',(-9.71741897707961,-0.0761083569579073,
14.4654963018055));
#29284=CARTESIAN_POINT('Ctrl Pts',(-9.69220224865988,-0.348998786067701,
14.4761979768309));
#29285=CARTESIAN_POINT('Ctrl Pts',(-9.49058638632123,-0.788683034815797,
14.4946176254726));
#29286=CARTESIAN_POINT('Ctrl Pts',(-9.00873218868954,-1.159514501144,14.5177715463217));
#29287=CARTESIAN_POINT('Ctrl Pts',(-8.40956988800579,-1.26297454963044,
14.5409254671708));
#29288=CARTESIAN_POINT('Ctrl Pts',(-7.8312597864405,-1.07520641969046,14.5640793880199));
#29289=CARTESIAN_POINT('Ctrl Pts',(-7.40715389611314,-0.639507397443362,
14.587233308869));
#29290=CARTESIAN_POINT('Ctrl Pts',(-7.23504641717748,-0.0563449330507459,
14.6103872297181));
#29291=CARTESIAN_POINT('Ctrl Pts',(-7.35462346018219,0.539810059387775,
14.6335411505671));
#29292=CARTESIAN_POINT('Ctrl Pts',(-7.73831186108132,1.01149073013163,14.6566950714162));
#29293=CARTESIAN_POINT('Ctrl Pts',(-8.29763725271243,1.24993265293153,14.6798489922653));
#29294=CARTESIAN_POINT('Ctrl Pts',(-8.9036252902427,1.20015371633275,14.7030029131144));
#29295=CARTESIAN_POINT('Ctrl Pts',(-9.4165417311248,0.873632402118881,14.7261568339635));
#29296=CARTESIAN_POINT('Ctrl Pts',(-9.6749061703283,0.421305628158093,14.7459933963909));
#29297=CARTESIAN_POINT('Ctrl Pts',(-9.71732882388252,0.112217516229114,
14.7581119852019));
#29298=CARTESIAN_POINT('Ctrl Pts',(-9.71736702302461,-1.11660450847831E-5,
14.7625126003965));
#29299=CARTESIAN_POINT('Origin',(-8.5,0.,13.1374873996035));
#29300=CARTESIAN_POINT('',(-9.7173946780644,-2.21442813102546E-5,14.1625126003965));
#29301=CARTESIAN_POINT('',(-9.71752512830443,-1.58793609722743E-5,14.1874873996035));
#29302=CARTESIAN_POINT('',(-9.71745,1.55202226700376E-15,13.1374873996035));
#29303=CARTESIAN_POINT('Ctrl Pts',(-9.71752512830443,-1.58793609723457E-5,
14.1874873996035));
#29304=CARTESIAN_POINT('Ctrl Pts',(-9.71753716083669,-0.0180768552027482,
14.1881958564963));
#29305=CARTESIAN_POINT('Ctrl Pts',(-9.71285049282718,-0.232888982065844,
14.1966222870055));
#29306=CARTESIAN_POINT('Ctrl Pts',(-9.59284608170875,-0.639507384465213,
14.212766691131));
#29307=CARTESIAN_POINT('Ctrl Pts',(-9.16874019998817,-1.07520639787033,
14.2359206119801));
#29308=CARTESIAN_POINT('Ctrl Pts',(-8.59043011015904,-1.26297452399975,
14.2590745328292));
#29309=CARTESIAN_POINT('Ctrl Pts',(-7.99126782163464,-1.15951447761293,
14.2822284536783));
#29310=CARTESIAN_POINT('Ctrl Pts',(-7.50941363378165,-0.788683018810342,
14.3053823745274));
#29311=CARTESIAN_POINT('Ctrl Pts',(-7.25597787533851,-0.235989843955851,
14.3285362953765));
#29312=CARTESIAN_POINT('Ctrl Pts',(-7.28940007250277,0.371120019187095,
14.3516902162256));
#29313=CARTESIAN_POINT('Ctrl Pts',(-7.60197343054782,0.892653647085789,
14.3748441370747));
#29314=CARTESIAN_POINT('Ctrl Pts',(-8.12162193676524,1.20835106420286,14.3979980579237));
#29315=CARTESIAN_POINT('Ctrl Pts',(-8.72852030415086,1.24541588382723,14.4211519787728));
#29316=CARTESIAN_POINT('Ctrl Pts',(-9.28272437778932,0.995301362156251,
14.4443058996219));
#29317=CARTESIAN_POINT('Ctrl Pts',(-9.63962047130265,0.537267975635789,
14.4664177065655));
#29318=CARTESIAN_POINT('Ctrl Pts',(-9.71736302924274,0.170176884784988,
14.4808115398927));
#29319=CARTESIAN_POINT('Ctrl Pts',(-9.71750538188158,-2.14937348604928E-5,
14.4874873996035));
#29320=CARTESIAN_POINT('Ctrl Pts',(-9.7173946780644,-2.21442813102893E-5,
14.1625126003965));
#29321=CARTESIAN_POINT('Ctrl Pts',(-9.71744185026584,-0.0676016943959369,
14.1651626447928));
#29322=CARTESIAN_POINT('Ctrl Pts',(-9.69577189929841,-0.331969587358445,
14.1755306628055));
#29323=CARTESIAN_POINT('Ctrl Pts',(-9.50690167961977,-0.767744309864743,
14.1936166544345));
#29324=CARTESIAN_POINT('Ctrl Pts',(-9.03292701443594,-1.14859527930365,
14.2167705752836));
#29325=CARTESIAN_POINT('Ctrl Pts',(-8.43606518260107,-1.26459268432005,
14.2399244961327));
#29326=CARTESIAN_POINT('Ctrl Pts',(-7.85394602357466,-1.08898878677709,
14.2630784169817));
#29327=CARTESIAN_POINT('Ctrl Pts',(-7.4207998764838,-0.662275933111461,
14.2862323378308));
#29328=CARTESIAN_POINT('Ctrl Pts',(-7.23650552633111,-0.0828494609134307,
14.3093862586799));
#29329=CARTESIAN_POINT('Ctrl Pts',(-7.3435592434188,0.515681194822054,14.332540179529));
#29330=CARTESIAN_POINT('Ctrl Pts',(-7.71727560632613,0.995301382354801,
14.3556941003781));
#29331=CARTESIAN_POINT('Ctrl Pts',(-8.27147969121155,1.24541590910158,14.3788480212272));
#29332=CARTESIAN_POINT('Ctrl Pts',(-8.87837807091352,1.20835108872504,14.4020019420763));
#29333=CARTESIAN_POINT('Ctrl Pts',(-9.39802658767663,0.892653665201231,
14.4251558629254));
#29334=CARTESIAN_POINT('Ctrl Pts',(-9.67032057157381,0.438326814809805,
14.4453260823654));
#29335=CARTESIAN_POINT('Ctrl Pts',(-9.71731427489874,0.120717436282016,
14.4577783281892));
#29336=CARTESIAN_POINT('Ctrl Pts',(-9.717378500128,-1.72188158990352E-5,
14.4625126003965));
#29337=CARTESIAN_POINT('Origin',(-8.5,0.,13.1374873996035));
#29338=CARTESIAN_POINT('',(-9.7174151537438,-2.95534814070963E-5,13.8625126003965));
#29339=CARTESIAN_POINT('',(-9.71753927955743,-8.82872242793887E-6,13.8874873996035));
#29340=CARTESIAN_POINT('',(-9.71745,1.55202226700376E-15,13.1374873996035));
#29341=CARTESIAN_POINT('',(-8.81478889550441,1.17604951161383,13.8));
#29342=CARTESIAN_POINT('Ctrl Pts',(-8.81478889550439,1.17604951161383,13.8));
#29343=CARTESIAN_POINT('Ctrl Pts',(-9.00489125583826,1.12516550422186,13.8077179736164));
#29344=CARTESIAN_POINT('Ctrl Pts',(-9.35978714971093,0.929517388355175,
13.8231539208491));
#29345=CARTESIAN_POINT('Ctrl Pts',(-9.6605571008421,0.472340818518349,13.8439914543146));
#29346=CARTESIAN_POINT('Ctrl Pts',(-9.71730301126828,0.137708208335554,
13.8571110141637));
#29347=CARTESIAN_POINT('Ctrl Pts',(-9.7174151537438,-2.95534814072282E-5,
13.8625126003965));
#29348=CARTESIAN_POINT('',(-8.18517792464733,1.17607853534586,13.8));
#29349=CARTESIAN_POINT('Origin',(-8.5,0.,13.8));
#29350=CARTESIAN_POINT('Ctrl Pts',(-8.18517792464733,1.17607853534586,13.8));
#29351=CARTESIAN_POINT('Ctrl Pts',(-8.34243071691597,1.21801500002725,13.8063833455655));
#29352=CARTESIAN_POINT('Ctrl Pts',(-8.7086380547407,1.24083318474607,13.8204846647474));
#29353=CARTESIAN_POINT('Ctrl Pts',(-9.24031697072028,1.02723635681965,13.8423039575456));
#29354=CARTESIAN_POINT('Ctrl Pts',(-9.62743942353789,0.571204689714611,
13.8650830785146));
#29355=CARTESIAN_POINT('Ctrl Pts',(-9.71746304864376,0.187187256572491,
13.8801442258672));
#29356=CARTESIAN_POINT('Ctrl Pts',(-9.71753927955742,-8.82872242803645E-6,
13.8874873996035));
#29357=CARTESIAN_POINT('Origin',(-8.5,0.,13.1374873996035));
#29358=CARTESIAN_POINT('Ctrl Pts',(-9.71753927955742,-8.82872242803645E-6,
13.8874873996035));
#29359=CARTESIAN_POINT('Ctrl Pts',(-9.71754317042782,-0.00956342634534076,
13.8878621994836));
#29360=CARTESIAN_POINT('Ctrl Pts',(-9.71516252585584,-0.215866768863219,
13.8959549729801));
#29361=CARTESIAN_POINT('Ctrl Pts',(-9.60601178848326,-0.616457875299982,
13.9117657200929));
#29362=CARTESIAN_POINT('Ctrl Pts',(-9.19113252777601,-1.06095145651566,
13.934919640942));
#29363=CARTESIAN_POINT('Ctrl Pts',(-8.61688566499978,-1.26080134768798,
13.9580735617911));
#29364=CARTESIAN_POINT('Ctrl Pts',(-8.0156862255606,-1.16992410182742,13.9812274826402));
#29365=CARTESIAN_POINT('Ctrl Pts',(-7.52616427574063,-0.809275132274592,
14.0043814034892));
#29366=CARTESIAN_POINT('Ctrl Pts',(-7.26119823647443,-0.262016113511643,
14.0275353243383));
#29367=CARTESIAN_POINT('Ctrl Pts',(-7.28188639587083,0.345660960504597,
14.0506892451874));
#29368=CARTESIAN_POINT('Ctrl Pts',(-7.5834582874758,0.873632384391611,14.0738431660365));
#29369=CARTESIAN_POINT('Ctrl Pts',(-8.09637471794825,1.2001536919759,14.0969970868856));
#29370=CARTESIAN_POINT('Ctrl Pts',(-8.7023627431809,1.24993262756601,14.1201510077347));
#29371=CARTESIAN_POINT('Ctrl Pts',(-9.26168812346101,1.01149070960429,14.1433049285838));
#29372=CARTESIAN_POINT('Ctrl Pts',(-9.63363653142959,0.554242395239179,
14.16575039254));
#29373=CARTESIAN_POINT('Ctrl Pts',(-9.71740607767908,0.178680543088794,
14.1804778828799));
#29374=CARTESIAN_POINT('Ctrl Pts',(-9.71752512830443,-1.58793609723457E-5,
14.1874873996035));
#29375=CARTESIAN_POINT('Ctrl Pts',(-9.7174151537438,-2.95534814072282E-5,
13.8625126003965));
#29376=CARTESIAN_POINT('Ctrl Pts',(-9.71746324432392,-0.05909627943313,
13.8648289877801));
#29377=CARTESIAN_POINT('Ctrl Pts',(-9.69914882474038,-0.314937855799663,
13.87486334878));
#29378=CARTESIAN_POINT('Ctrl Pts',(-9.52277717161101,-0.746471281904888,
13.8926156833963));
#29379=CARTESIAN_POINT('Ctrl Pts',(-9.05688631633702,-1.13717009764717,
13.9157696042454));
#29380=CARTESIAN_POINT('Ctrl Pts',(-8.46258916536876,-1.26565565606363,
13.9389235250945));
#29381=CARTESIAN_POINT('Ctrl Pts',(-7.87691591618916,-1.10229229667761,
13.9620774459436));
#29382=CARTESIAN_POINT('Ctrl Pts',(-7.43492027566404,-0.684753533801549,
13.9852313667927));
#29383=CARTESIAN_POINT('Ctrl Pts',(-7.23851986425691,-0.109317520883414,
14.0083852876418));
#29384=CARTESIAN_POINT('Ctrl Pts',(-7.33300329226471,0.491325669494413,
14.0315392084909));
#29385=CARTESIAN_POINT('Ctrl Pts',(-7.6965833349978,0.978674626363476,14.05469312934));
#29386=CARTESIAN_POINT('Ctrl Pts',(-8.24542256676704,1.24035181775585,14.077847050189));
#29387=CARTESIAN_POINT('Ctrl Pts',(-8.8529645573119,1.21601741100899,14.1010009710381));
#29388=CARTESIAN_POINT('Ctrl Pts',(-9.37911677604257,0.911282619288843,
14.1241548918872));
#29389=CARTESIAN_POINT('Ctrl Pts',(-9.66553572491195,0.455344208231389,
14.14465876834));
#29390=CARTESIAN_POINT('Ctrl Pts',(-9.71730446622554,0.12921658741071,14.1574446711764));
#29391=CARTESIAN_POINT('Ctrl Pts',(-9.7173946780644,-2.21442813102893E-5,
14.1625126003965));
#29392=CARTESIAN_POINT('Ctrl Pts',(-7.70661869325992,-0.687936125025717,
13.8));
#29393=CARTESIAN_POINT('Ctrl Pts',(-7.59541735366082,-0.559690113640457,
13.8077179736164));
#29394=CARTESIAN_POINT('Ctrl Pts',(-7.43647625507643,-0.24836978034843,
13.8231539208491));
#29395=CARTESIAN_POINT('Ctrl Pts',(-7.44330893610161,0.27607510271298,13.8463078416982));
#29396=CARTESIAN_POINT('Ctrl Pts',(-7.69382532330059,0.736799251308305,
13.8694617625473));
#29397=CARTESIAN_POINT('Ctrl Pts',(-8.1302326392485,1.02765925647027,13.8926156833963));
#29398=CARTESIAN_POINT('Ctrl Pts',(-8.65190777128926,1.08153816631997,13.9157696042454));
#29399=CARTESIAN_POINT('Ctrl Pts',(-9.13855341160078,0.886033018437155,
13.9389235250945));
#29400=CARTESIAN_POINT('Ctrl Pts',(-9.47795624898969,0.486215233061711,
13.9620774459436));
#29401=CARTESIAN_POINT('Ctrl Pts',(-9.59185274523544,-0.0257170490500127,
13.9852313667927));
#29402=CARTESIAN_POINT('Ctrl Pts',(-9.45398002306975,-0.531719918561346,
14.0083852876418));
#29403=CARTESIAN_POINT('Ctrl Pts',(-9.09612983483313,-0.915113659277255,
14.0315392084909));
#29404=CARTESIAN_POINT('Ctrl Pts',(-8.60081862648673,-1.08749229554162,
14.05469312934));
#29405=CARTESIAN_POINT('Ctrl Pts',(-8.08225972767768,-1.009106985362,14.077847050189));
#29406=CARTESIAN_POINT('Ctrl Pts',(-7.66002719286643,-0.698032622614111,
14.1010009710381));
#29407=CARTESIAN_POINT('Ctrl Pts',(-7.43148323801536,-0.225999524250339,
14.1241548918872));
#29408=CARTESIAN_POINT('Ctrl Pts',(-7.44932761452541,0.298146597088897,
14.1473088127363));
#29409=CARTESIAN_POINT('Ctrl Pts',(-7.70944560160856,0.753543362642926,
14.1704627335854));
#29410=CARTESIAN_POINT('Ctrl Pts',(-8.151856824771,1.03518123285875,14.1936166544345));
#29411=CARTESIAN_POINT('Ctrl Pts',(-8.67454607303319,1.07811758364374,14.2167705752836));
#29412=CARTESIAN_POINT('Ctrl Pts',(-9.15698689756985,0.872451759132174,
14.2399244961327));
#29413=CARTESIAN_POINT('Ctrl Pts',(-9.48793369752679,0.465608059353192,
14.2630784169817));
#29414=CARTESIAN_POINT('Ctrl Pts',(-9.59107374460138,-0.0485997888996519,
14.2862323378308));
#29415=CARTESIAN_POINT('Ctrl Pts',(-9.44262406702728,-0.551601055014103,
14.3093862586799));
#29416=CARTESIAN_POINT('Ctrl Pts',(-9.07681554397107,-0.927409124320201,
14.332540179529));
#29417=CARTESIAN_POINT('Ctrl Pts',(-8.57799963750299,-1.08936674824603,
14.3556941003781));
#29418=CARTESIAN_POINT('Ctrl Pts',(-8.06119786397678,-1.00012826230345,
14.3788480212272));
#29419=CARTESIAN_POINT('Ctrl Pts',(-7.64557908483643,-0.680271089615787,
14.4020019420763));
#29420=CARTESIAN_POINT('Ctrl Pts',(-7.42698046481824,-0.203550811234991,
14.4251558629254));
#29421=CARTESIAN_POINT('Ctrl Pts',(-7.45580846534574,0.320106067722181,
14.4483097837745));
#29422=CARTESIAN_POINT('Ctrl Pts',(-7.72541566340981,0.769949973144512,
14.4714637046235));
#29423=CARTESIAN_POINT('Ctrl Pts',(-8.1736335749289,1.0422517988578,14.4946176254726));
#29424=CARTESIAN_POINT('Ctrl Pts',(-8.69710803021792,1.07422170898761,14.5177715463217));
#29425=CARTESIAN_POINT('Ctrl Pts',(-9.17513152007603,0.858487790381764,
14.5409254671708));
#29426=CARTESIAN_POINT('Ctrl Pts',(-9.49747703301279,0.444795935515361,
14.5640793880199));
#29427=CARTESIAN_POINT('Ctrl Pts',(-9.58981520380618,-0.0714610186370064,
14.587233308869));
#29428=CARTESIAN_POINT('Ctrl Pts',(-9.43085385576899,-0.571239840031833,
14.6103872297181));
#29429=CARTESIAN_POINT('Ctrl Pts',(-9.05724774477506,-0.939296974650035,
14.6335411505671));
#29430=CARTESIAN_POINT('Ctrl Pts',(-8.55514637183314,-1.09076245501251,
14.6566950714162));
#29431=CARTESIAN_POINT('Ctrl Pts',(-8.04032884594654,-0.990709990816833,
14.6798489922653));
#29432=CARTESIAN_POINT('Ctrl Pts',(-7.63150648296805,-0.662210590518583,
14.7030029131144));
#29433=CARTESIAN_POINT('Ctrl Pts',(-7.42294926740862,-0.181012639402946,
14.7261568339635));
#29434=CARTESIAN_POINT('Ctrl Pts',(-7.46274822360797,0.341924856256622,
14.7493107548126));
#29435=CARTESIAN_POINT('Ctrl Pts',(-7.74172614251806,0.786018201228814,
14.7724646756617));
#29436=CARTESIAN_POINT('Ctrl Pts',(-8.19555376064367,1.04886431262541,14.7956185965108));
#29437=CARTESIAN_POINT('Ctrl Pts',(-8.71958335635884,1.06985372487855,14.8187725173598));
#29438=CARTESIAN_POINT('Ctrl Pts',(-9.19297944295253,0.844146539384165,
14.8419264382089));
#29439=CARTESIAN_POINT('Ctrl Pts',(-9.50658196876613,0.423788307447097,
14.865080359058));
#29440=CARTESIAN_POINT('Ctrl Pts',(-9.58807775575186,-0.0942907930237714,
14.8882342799071));
#29441=CARTESIAN_POINT('Ctrl Pts',(-9.41867443891702,-0.590627682360479,
14.9113882007562));
#29442=CARTESIAN_POINT('Ctrl Pts',(-9.03743528136299,-0.950771789729547,
14.9345421216053));
#29443=CARTESIAN_POINT('Ctrl Pts',(-8.53226836097154,-1.09167931285156,
14.9576960424544));
#29444=CARTESIAN_POINT('Ctrl Pts',(-8.01966297638898,-0.980855300201485,
14.9808499633034));
#29445=CARTESIAN_POINT('Ctrl Pts',(-7.617813225467,-0.643861742399126,15.0040038841525));
#29446=CARTESIAN_POINT('Ctrl Pts',(-7.41939690868525,-0.158390988130214,
15.0271578050016));
#29447=CARTESIAN_POINT('Ctrl Pts',(-7.47013353180666,0.363577398295972,
15.0503117258507));
#29448=CARTESIAN_POINT('Ctrl Pts',(-7.75839866563354,0.801746696078297,
15.0734656466998));
#29449=CARTESIAN_POINT('Ctrl Pts',(-8.06451081542916,0.970500879693927,
15.0889015939325));
#29450=CARTESIAN_POINT('Ctrl Pts',(-8.22848181102371,1.01439039972539,15.0966195675489));
#29451=CARTESIAN_POINT('Ctrl Pts',(-7.66447275106935,-0.724480616192607,
13.7677934774837));
#29452=CARTESIAN_POINT('Ctrl Pts',(-7.54736418225973,-0.589421929822323,
13.7755114511001));
#29453=CARTESIAN_POINT('Ctrl Pts',(-7.37997982657345,-0.261563661166546,
13.7909473983328));
#29454=CARTESIAN_POINT('Ctrl Pts',(-7.38717547276688,0.290740743584966,
13.8141013191819));
#29455=CARTESIAN_POINT('Ctrl Pts',(-7.65099977267187,0.775939445799765,
13.837255240031));
#29456=CARTESIAN_POINT('Ctrl Pts',(-8.11058988528164,1.08225049431121,13.8604091608801));
#29457=CARTESIAN_POINT('Ctrl Pts',(-8.65997740450681,1.13899155556342,13.8835630817291));
#29458=CARTESIAN_POINT('Ctrl Pts',(-9.17247459797395,0.933100797897987,
13.9067170025782));
#29459=CARTESIAN_POINT('Ctrl Pts',(-9.52990716740014,0.512043922155726,
13.9298709234273));
#29460=CARTESIAN_POINT('Ctrl Pts',(-9.64985406476538,-0.027083188198195,
13.9530248442764));
#29461=CARTESIAN_POINT('Ctrl Pts',(-9.50465727820759,-0.559965904140891,
13.9761787651255));
#29462=CARTESIAN_POINT('Ctrl Pts',(-9.12779739914742,-0.963726258356724,
13.9993326859746));
#29463=CARTESIAN_POINT('Ctrl Pts',(-8.60617430599108,-1.14526197959041,
14.0224866068237));
#29464=CARTESIAN_POINT('Ctrl Pts',(-8.06006856030532,-1.06271269085048,
14.0456405276728));
#29465=CARTESIAN_POINT('Ctrl Pts',(-7.61540622049117,-0.735113459167605,
14.0687944485218));
#29466=CARTESIAN_POINT('Ctrl Pts',(-7.37472157083505,-0.238005054004107,
14.0919483693709));
#29467=CARTESIAN_POINT('Ctrl Pts',(-7.39351387497389,0.313984718227464,
14.11510229022));
#29468=CARTESIAN_POINT('Ctrl Pts',(-7.66744983023097,0.793573036559154,
14.1382562110691));
#29469=CARTESIAN_POINT('Ctrl Pts',(-8.13336278916342,1.09017205256447,14.1614101319182));
#29470=CARTESIAN_POINT('Ctrl Pts',(-8.68381829641576,1.13538926495116,14.1845640527673));
#29471=CARTESIAN_POINT('Ctrl Pts',(-9.19188730620024,0.918798075956213,
14.2077179736164));
#29472=CARTESIAN_POINT('Ctrl Pts',(-9.54041463720908,0.490342055713144,
14.2308718944655));
#29473=CARTESIAN_POINT('Ctrl Pts',(-9.64903368211814,-0.0511815032355429,
14.2540258153145));
#29474=CARTESIAN_POINT('Ctrl Pts',(-9.4926980719211,-0.580903164831139,
14.2771797361636));
#29475=CARTESIAN_POINT('Ctrl Pts',(-9.10745709597677,-0.976674882170243,
14.3003336570127));
#29476=CARTESIAN_POINT('Ctrl Pts',(-8.58214312838834,-1.1472360068306,14.3234875778618));
#29477=CARTESIAN_POINT('Ctrl Pts',(-8.03788784986273,-1.05325700073994,
14.3466414987109));
#29478=CARTESIAN_POINT('Ctrl Pts',(-7.6001906011515,-0.716408399347305,
14.36979541956));
#29479=CARTESIAN_POINT('Ctrl Pts',(-7.36997960165833,-0.214363822141945,
14.3929493404091));
#29480=CARTESIAN_POINT('Ctrl Pts',(-7.40033900106474,0.337110718210485,
14.4161032612582));
#29481=CARTESIAN_POINT('Ctrl Pts',(-7.68426825245581,0.810851197791604,
14.4392571821072));
#29482=CARTESIAN_POINT('Ctrl Pts',(-8.15629636220767,1.09761822063948,14.4624111029563));
#29483=CARTESIAN_POINT('Ctrl Pts',(-8.70757878819557,1.13128643393415,14.4855650238054));
#29484=CARTESIAN_POINT('Ctrl Pts',(-9.21099580598046,0.904092314306593,
14.5087189446545));
#29485=CARTESIAN_POINT('Ctrl Pts',(-9.55046493304603,0.468424351795872,
14.5318728655036));
#29486=CARTESIAN_POINT('Ctrl Pts',(-9.64770828521333,-0.0752571655020362,
14.5550267863527));
#29487=CARTESIAN_POINT('Ctrl Pts',(-9.48030260438434,-0.601585199911631,
14.5781807072018));
#29488=CARTESIAN_POINT('Ctrl Pts',(-9.08684981762149,-0.989194237992473,
14.6013346280509));
#29489=CARTESIAN_POINT('Ctrl Pts',(-8.55807585325594,-1.14870585622711,
14.6244885488999));
#29490=CARTESIAN_POINT('Ctrl Pts',(-8.01591022942404,-1.04333841254276,
14.647642469749));
#29491=CARTESIAN_POINT('Ctrl Pts',(-7.58537043558358,-0.697388491773475,
14.6707963905981));
#29492=CARTESIAN_POINT('Ctrl Pts',(-7.36573425928267,-0.190628379238543,
14.6939503114472));
#29493=CARTESIAN_POINT('Ctrl Pts',(-7.40764741264418,0.360088562790776,
14.7171042322963));
#29494=CARTESIAN_POINT('Ctrl Pts',(-7.70144517561027,0.827773001081413,
14.7402581531454));
#29495=CARTESIAN_POINT('Ctrl Pts',(-8.1793809903817,1.10458200386683,14.7634120739945));
#29496=CARTESIAN_POINT('Ctrl Pts',(-8.73124804692375,1.1266864141013,14.7865659948435));
#29497=CARTESIAN_POINT('Ctrl Pts',(-9.22979184487555,0.888989228450584,
14.8097199156926));
#29498=CARTESIAN_POINT('Ctrl Pts',(-9.56005354051264,0.446300758087122,
14.8328738365417));
#29499=CARTESIAN_POINT('Ctrl Pts',(-9.64587854057396,-0.0992997014491682,
14.8560277573908));
#29500=CARTESIAN_POINT('Ctrl Pts',(-9.46747619346509,-0.622002961744356,
14.8791816782399));
#29501=CARTESIAN_POINT('Ctrl Pts',(-9.06598487801604,-1.00127861733684,
14.902335599089));
#29502=CARTESIAN_POINT('Ctrl Pts',(-8.53398251841959,-1.14967141931943,
14.9254895199381));
#29503=CARTESIAN_POINT('Ctrl Pts',(-7.99414654909593,-1.03296022179267,
14.9486434407871));
#29504=CARTESIAN_POINT('Ctrl Pts',(-7.57094976588598,-0.678064917522287,
14.9717973616362));
#29505=CARTESIAN_POINT('Ctrl Pts',(-7.36199319242599,-0.166805022305877,
14.9949512824853));
#29506=CARTESIAN_POINT('Ctrl Pts',(-7.41542504263034,0.382891329542149,
15.0181052033344));
#29507=CARTESIAN_POINT('Ctrl Pts',(-7.71900337524653,0.844337023853018,
15.0412591241835));
#29508=CARTESIAN_POINT('Ctrl Pts',(-8.04137679167335,1.02205575453657,15.0566950714162));
#29509=CARTESIAN_POINT('Ctrl Pts',(-8.21405824218101,1.06827677035487,15.0644130450326));
#29510=CARTESIAN_POINT('Ctrl Pts',(-7.62232680887878,-0.761025107359497,
13.7355869549674));
#29511=CARTESIAN_POINT('Ctrl Pts',(-7.49931101085863,-0.619153746004188,
13.7433049285838));
#29512=CARTESIAN_POINT('Ctrl Pts',(-7.32348339807046,-0.274757541984661,
13.7587408758165));
#29513=CARTESIAN_POINT('Ctrl Pts',(-7.33104200943215,0.305406384456951,
13.7818947966656));
#29514=CARTESIAN_POINT('Ctrl Pts',(-7.60817422204316,0.815079640291225,
13.8050487175147));
#29515=CARTESIAN_POINT('Ctrl Pts',(-8.09094713131479,1.13684173215214,13.8282026383638));
#29516=CARTESIAN_POINT('Ctrl Pts',(-8.66804703772436,1.19644494480687,13.8513565592128));
#29517=CARTESIAN_POINT('Ctrl Pts',(-9.20639578434712,0.980168577358818,
13.8745104800619));
#29518=CARTESIAN_POINT('Ctrl Pts',(-9.58185808581058,0.537872611249743,
13.897664400911));
#29519=CARTESIAN_POINT('Ctrl Pts',(-9.70785538429531,-0.0284493273463784,
13.9208183217601));
#29520=CARTESIAN_POINT('Ctrl Pts',(-9.55533453334542,-0.588211889720436,
13.9439722426092));
#29521=CARTESIAN_POINT('Ctrl Pts',(-9.15946496346172,-1.01233885743619,
13.9671261634583));
#29522=CARTESIAN_POINT('Ctrl Pts',(-8.61152998549543,-1.20303166363919,
13.9902800843074));
#29523=CARTESIAN_POINT('Ctrl Pts',(-8.03787739293296,-1.11631839633895,
14.0134340051565));
#29524=CARTESIAN_POINT('Ctrl Pts',(-7.5707852481159,-0.772194295721099,
14.0365879260055));
#29525=CARTESIAN_POINT('Ctrl Pts',(-7.31795990365474,-0.250010583757875,
14.0597418468546));
#29526=CARTESIAN_POINT('Ctrl Pts',(-7.33770013542236,0.32982283936603,14.0828957677037));
#29527=CARTESIAN_POINT('Ctrl Pts',(-7.62545405885339,0.833602710475383,
14.1060496885528));
#29528=CARTESIAN_POINT('Ctrl Pts',(-8.11486875355584,1.14516287227018,14.1292036094019));
#29529=CARTESIAN_POINT('Ctrl Pts',(-8.69309051979833,1.19266094625859,14.152357530251));
#29530=CARTESIAN_POINT('Ctrl Pts',(-9.22678771483062,0.965144392780252,
14.1755114511001));
#29531=CARTESIAN_POINT('Ctrl Pts',(-9.59289557689136,0.515076052073095,
14.1986653719492));
#29532=CARTESIAN_POINT('Ctrl Pts',(-9.70699361963491,-0.0537632175714332,
14.2218192927982));
#29533=CARTESIAN_POINT('Ctrl Pts',(-9.54277207681493,-0.610205274648177,
14.2449732136473));
#29534=CARTESIAN_POINT('Ctrl Pts',(-9.13809864798247,-1.02594064002028,
14.2681271344964));
#29535=CARTESIAN_POINT('Ctrl Pts',(-8.58628661927369,-1.20510526541518,
14.2912810553455));
#29536=CARTESIAN_POINT('Ctrl Pts',(-8.01457783574869,-1.10638573917644,
14.3144349761946));
#29537=CARTESIAN_POINT('Ctrl Pts',(-7.55480211746658,-0.752545709078824,
14.3375888970437));
#29538=CARTESIAN_POINT('Ctrl Pts',(-7.31297873849841,-0.225176833048898,
14.3607428178928));
#29539=CARTESIAN_POINT('Ctrl Pts',(-7.34486953678376,0.35411536869879,14.3838967387419));
#29540=CARTESIAN_POINT('Ctrl Pts',(-7.64312084150182,0.851752422438698,
14.4070506595909));
#29541=CARTESIAN_POINT('Ctrl Pts',(-8.13895914948646,1.15298464242117,14.43020458044));
#29542=CARTESIAN_POINT('Ctrl Pts',(-8.71804954617321,1.18835115888069,14.4533585012891));
#29543=CARTESIAN_POINT('Ctrl Pts',(-9.24686009188489,0.949696838231421,
14.4765124221382));
#29544=CARTESIAN_POINT('Ctrl Pts',(-9.60345283307926,0.492052768076384,
14.4996663429873));
#29545=CARTESIAN_POINT('Ctrl Pts',(-9.70560136662048,-0.0790533123670655,
14.5228202638364));
#29546=CARTESIAN_POINT('Ctrl Pts',(-9.52975135299969,-0.63193055979143,
14.5459741846855));
#29547=CARTESIAN_POINT('Ctrl Pts',(-9.11645189046791,-1.03909150133491,
14.5691281055345));
#29548=CARTESIAN_POINT('Ctrl Pts',(-8.56100533467875,-1.2066492574417,14.5922820263836));
#29549=CARTESIAN_POINT('Ctrl Pts',(-7.99149161290154,-1.09596683426869,
14.6154359472327));
#29550=CARTESIAN_POINT('Ctrl Pts',(-7.53923438819912,-0.732566393028366,
14.6385898680818));
#29551=CARTESIAN_POINT('Ctrl Pts',(-7.30851925115672,-0.200244119074141,
14.6617437889309));
#29552=CARTESIAN_POINT('Ctrl Pts',(-7.3525466016804,0.37825226932493,14.68489770978));
#29553=CARTESIAN_POINT('Ctrl Pts',(-7.66116420870248,0.869527800934012,
14.7080516306291));
#29554=CARTESIAN_POINT('Ctrl Pts',(-8.16320822011973,1.16029969510826,14.7312055514782));
#29555=CARTESIAN_POINT('Ctrl Pts',(-8.74291273748866,1.18351910332405,14.7543594723272));
#29556=CARTESIAN_POINT('Ctrl Pts',(-9.26660424679858,0.933831917517003,
14.7775133931763));
#29557=CARTESIAN_POINT('Ctrl Pts',(-9.61352511225915,0.468813208727148,
14.8006673140254));
#29558=CARTESIAN_POINT('Ctrl Pts',(-9.70367932539607,-0.104308609874565,
14.8238212348745));
#29559=CARTESIAN_POINT('Ctrl Pts',(-9.51627794801315,-0.653378241128233,
14.8469751557236));
#29560=CARTESIAN_POINT('Ctrl Pts',(-9.09453447466908,-1.05178544494412,
14.8701290765727));
#29561=CARTESIAN_POINT('Ctrl Pts',(-8.53569667586763,-1.20766352578729,
14.8932829974218));
#29562=CARTESIAN_POINT('Ctrl Pts',(-7.96863012180288,-1.08506514338386,
14.9164369182709));
#29563=CARTESIAN_POINT('Ctrl Pts',(-7.52408630630496,-0.712268092645449,
14.9395908391199));
#29564=CARTESIAN_POINT('Ctrl Pts',(-7.30458947616674,-0.175219056481539,
14.962744759969));
#29565=CARTESIAN_POINT('Ctrl Pts',(-7.36071655345402,0.402205260788326,
14.9858986808181));
#29566=CARTESIAN_POINT('Ctrl Pts',(-7.67960808485951,0.886927351627739,
15.0090526016672));
#29567=CARTESIAN_POINT('Ctrl Pts',(-8.01824276791754,1.07361062937921,15.0244885488999));
#29568=CARTESIAN_POINT('Ctrl Pts',(-8.1996346733383,1.12216314098435,15.0322065225163));
#29569=CARTESIAN_POINT('Ctrl Pts',(-7.58018086668821,-0.797569598526387,
13.7033804324511));
#29570=CARTESIAN_POINT('Ctrl Pts',(-7.45125783945754,-0.648885562186053,
13.7110984060675));
#29571=CARTESIAN_POINT('Ctrl Pts',(-7.26698696956747,-0.287951422802777,
13.7265343533002));
#29572=CARTESIAN_POINT('Ctrl Pts',(-7.27490854609742,0.320072025328937,
13.7496882741493));
#29573=CARTESIAN_POINT('Ctrl Pts',(-7.56534867141445,0.854219834782685,
13.7728421949984));
#29574=CARTESIAN_POINT('Ctrl Pts',(-8.07130437734794,1.19143296999308,13.7959961158475));
#29575=CARTESIAN_POINT('Ctrl Pts',(-8.67611667094192,1.25389833405033,13.8191500366966));
#29576=CARTESIAN_POINT('Ctrl Pts',(-9.24031697072028,1.02723635681965,13.8423039575456));
#29577=CARTESIAN_POINT('Ctrl Pts',(-9.63380900422103,0.563701300343758,
13.8654578783947));
#29578=CARTESIAN_POINT('Ctrl Pts',(-9.76585670382525,-0.0298154664945606,
13.8886117992438));
#29579=CARTESIAN_POINT('Ctrl Pts',(-9.60601178848326,-0.616457875299982,
13.9117657200929));
#29580=CARTESIAN_POINT('Ctrl Pts',(-9.19113252777601,-1.06095145651566,
13.934919640942));
#29581=CARTESIAN_POINT('Ctrl Pts',(-8.61688566499978,-1.26080134768798,
13.9580735617911));
#29582=CARTESIAN_POINT('Ctrl Pts',(-8.0156862255606,-1.16992410182742,13.9812274826402));
#29583=CARTESIAN_POINT('Ctrl Pts',(-7.52616427574063,-0.809275132274592,
14.0043814034892));
#29584=CARTESIAN_POINT('Ctrl Pts',(-7.26119823647443,-0.262016113511643,
14.0275353243383));
#29585=CARTESIAN_POINT('Ctrl Pts',(-7.28188639587083,0.345660960504597,
14.0506892451874));
#29586=CARTESIAN_POINT('Ctrl Pts',(-7.5834582874758,0.873632384391611,14.0738431660365));
#29587=CARTESIAN_POINT('Ctrl Pts',(-8.09637471794825,1.2001536919759,14.0969970868856));
#29588=CARTESIAN_POINT('Ctrl Pts',(-8.7023627431809,1.24993262756601,14.1201510077347));
#29589=CARTESIAN_POINT('Ctrl Pts',(-9.26168812346101,1.01149070960429,14.1433049285838));
#29590=CARTESIAN_POINT('Ctrl Pts',(-9.64537651657365,0.539810048433048,
14.1664588494329));
#29591=CARTESIAN_POINT('Ctrl Pts',(-9.76495355715166,-0.0563449319073242,
14.1896127702819));
#29592=CARTESIAN_POINT('Ctrl Pts',(-9.59284608170875,-0.639507384465213,
14.212766691131));
#29593=CARTESIAN_POINT('Ctrl Pts',(-9.16874019998817,-1.07520639787033,
14.2359206119801));
#29594=CARTESIAN_POINT('Ctrl Pts',(-8.59043011015904,-1.26297452399975,
14.2590745328292));
#29595=CARTESIAN_POINT('Ctrl Pts',(-7.99126782163464,-1.15951447761293,
14.2822284536783));
#29596=CARTESIAN_POINT('Ctrl Pts',(-7.50941363378165,-0.788683018810342,
14.3053823745274));
#29597=CARTESIAN_POINT('Ctrl Pts',(-7.25597787533851,-0.235989843955851,
14.3285362953765));
#29598=CARTESIAN_POINT('Ctrl Pts',(-7.28940007250277,0.371120019187095,
14.3516902162256));
#29599=CARTESIAN_POINT('Ctrl Pts',(-7.60197343054782,0.892653647085789,
14.3748441370747));
#29600=CARTESIAN_POINT('Ctrl Pts',(-8.12162193676524,1.20835106420286,14.3979980579237));
#29601=CARTESIAN_POINT('Ctrl Pts',(-8.72852030415086,1.24541588382723,14.4211519787728));
#29602=CARTESIAN_POINT('Ctrl Pts',(-9.28272437778932,0.995301362156251,
14.4443058996219));
#29603=CARTESIAN_POINT('Ctrl Pts',(-9.65644073311249,0.515681184356895,
14.467459820471));
#29604=CARTESIAN_POINT('Ctrl Pts',(-9.76349444802764,-0.0828494592320952,
14.4906137413201));
#29605=CARTESIAN_POINT('Ctrl Pts',(-9.57920010161505,-0.662275919671228,
14.5137676621692));
#29606=CARTESIAN_POINT('Ctrl Pts',(-9.14605396331434,-1.08898876467735,
14.5369215830183));
#29607=CARTESIAN_POINT('Ctrl Pts',(-8.56393481610157,-1.2645926586563,14.5600755038673));
#29608=CARTESIAN_POINT('Ctrl Pts',(-7.96707299637902,-1.14859525599462,
14.5832294247164));
#29609=CARTESIAN_POINT('Ctrl Pts',(-7.49309834081465,-0.767744294283258,
14.6063833455655));
#29610=CARTESIAN_POINT('Ctrl Pts',(-7.25130424303077,-0.209859858909738,
14.6295372664146));
#29611=CARTESIAN_POINT('Ctrl Pts',(-7.29744579071662,0.396415975859085,
14.6526911872637));
#29612=CARTESIAN_POINT('Ctrl Pts',(-7.62088324179469,0.911282600786611,
14.6758451081128));
#29613=CARTESIAN_POINT('Ctrl Pts',(-8.14703544985776,1.21601738634968,14.6989990289619));
#29614=CARTESIAN_POINT('Ctrl Pts',(-8.75457742805358,1.2403517925468,14.722152949811));
#29615=CARTESIAN_POINT('Ctrl Pts',(-9.3034166487216,0.978674606583422,14.74530687066));
#29616=CARTESIAN_POINT('Ctrl Pts',(-9.66699668400565,0.491325659367174,
14.7684607915091));
#29617=CARTESIAN_POINT('Ctrl Pts',(-9.76148011021817,-0.109317518299962,
14.7916147123582));
#29618=CARTESIAN_POINT('Ctrl Pts',(-9.56507970256121,-0.68475352051211,
14.8147686332073));
#29619=CARTESIAN_POINT('Ctrl Pts',(-9.12308407132213,-1.10229227255141,
14.8379225540564));
#29620=CARTESIAN_POINT('Ctrl Pts',(-8.53741083331568,-1.26565563225515,
14.8610764749055));
#29621=CARTESIAN_POINT('Ctrl Pts',(-7.94311369450983,-1.13717006497505,
14.8842303957546));
#29622=CARTESIAN_POINT('Ctrl Pts',(-7.47722284672394,-0.74647126776861,
14.9073843166036));
#29623=CARTESIAN_POINT('Ctrl Pts',(-7.24718575990748,-0.183633090657203,
14.9305382374527));
#29624=CARTESIAN_POINT('Ctrl Pts',(-7.3060080642777,0.421519192034503,14.9536921583018));
#29625=CARTESIAN_POINT('Ctrl Pts',(-7.64021279447249,0.92951767940246,14.9768460791509));
#29626=CARTESIAN_POINT('Ctrl Pts',(-7.99510874416173,1.12516550422186,14.9922820263836));
#29627=CARTESIAN_POINT('Ctrl Pts',(-8.18521110449559,1.17604951161383,15.));
#29628=CARTESIAN_POINT('Ctrl Pts',(-8.18521110449559,1.17604951161383,15.));
#29629=CARTESIAN_POINT('Ctrl Pts',(-8.13719918410313,1.15963858074114,15.));
#29630=CARTESIAN_POINT('Ctrl Pts',(-8.09039143005571,1.14022106600632,15.));
#29631=CARTESIAN_POINT('Ctrl Pts',(-8.04502571698153,1.11798781401985,15.));
#29632=CARTESIAN_POINT('Ctrl Pts',(-7.99968245369021,1.09576556443245,15.));
#29633=CARTESIAN_POINT('Ctrl Pts',(-7.95577890640656,1.07072966351069,15.));
#29634=CARTESIAN_POINT('Ctrl Pts',(-7.91357983441579,1.04302643998004,15.));
#29635=CARTESIAN_POINT('Ctrl Pts',(-7.87480106608641,1.01756860793323,15.));
#29636=CARTESIAN_POINT('Ctrl Pts',(-7.8374614440569,0.989857442508656,15.));
#29637=CARTESIAN_POINT('Ctrl Pts',(-7.80179646271021,0.959980963961019,
15.));
#29638=CARTESIAN_POINT('Ctrl Pts',(-7.79470070794682,0.954036865381321,
15.));
#29639=CARTESIAN_POINT('Ctrl Pts',(-7.78766969979432,0.94800553688181,15.));
#29640=CARTESIAN_POINT('Ctrl Pts',(-7.78071079958526,0.941892285934689,
15.));
#29641=CARTESIAN_POINT('Ctrl Pts',(-7.75269258257066,0.917278857583148,
15.));
#29642=CARTESIAN_POINT('Ctrl Pts',(-7.72591191331948,0.891400647665221,
15.));
#29643=CARTESIAN_POINT('Ctrl Pts',(-7.70047025475673,0.864321952622116,
15.));
#29644=CARTESIAN_POINT('Ctrl Pts',(-7.66652586503523,0.828193420536614,
15.));
#29645=CARTESIAN_POINT('Ctrl Pts',(-7.63496310561488,0.789928497182938,
15.));
#29646=CARTESIAN_POINT('Ctrl Pts',(-7.60593174101237,0.749793509612499,
15.));
#29647=CARTESIAN_POINT('Ctrl Pts',(-7.58573652511221,0.721874231609796,
15.));
#29648=CARTESIAN_POINT('Ctrl Pts',(-7.5667671232806,0.693049287271894,15.));
#29649=CARTESIAN_POINT('Ctrl Pts',(-7.54908765839019,0.663402582514798,
15.));
#29650=CARTESIAN_POINT('Ctrl Pts',(-7.53965695670849,0.64758823348654,15.));
#29651=CARTESIAN_POINT('Ctrl Pts',(-7.53059349991873,0.631539998511114,
15.));
#29652=CARTESIAN_POINT('Ctrl Pts',(-7.52190847036827,0.615270358408881,
15.));
#29653=CARTESIAN_POINT('Ctrl Pts',(-7.51748854481548,0.606990524977705,
15.));
#29654=CARTESIAN_POINT('Ctrl Pts',(-7.51316664579,0.598653347566876,15.));
#29655=CARTESIAN_POINT('Ctrl Pts',(-7.50894435340399,0.590260465682536,
15.));
#29656=CARTESIAN_POINT('Ctrl Pts',(-7.50442240551159,0.581271942132195,
15.));
#29657=CARTESIAN_POINT('Ctrl Pts',(-7.50001807492301,0.572226073963554,
15.));
#29658=CARTESIAN_POINT('Ctrl Pts',(-7.49573609254012,0.563132443556206,
15.));
#29659=CARTESIAN_POINT('Ctrl Pts',(-7.47506492170153,0.519233153254429,
15.));
#29660=CARTESIAN_POINT('Ctrl Pts',(-7.45721452036603,0.474169527752238,
15.));
#29661=CARTESIAN_POINT('Ctrl Pts',(-7.44233237690941,0.428189108276674,
15.));
#29662=CARTESIAN_POINT('Ctrl Pts',(-7.43702150858781,0.411780453574552,
15.));
#29663=CARTESIAN_POINT('Ctrl Pts',(-7.43208910475981,0.395254894640867,
15.));
#29664=CARTESIAN_POINT('Ctrl Pts',(-7.42754344368022,0.378623315021146,
15.));
#29665=CARTESIAN_POINT('Ctrl Pts',(-7.41562266198816,0.335007782237456,
15.));
#29666=CARTESIAN_POINT('Ctrl Pts',(-7.40635883556592,0.29066280905082,15.));
#29667=CARTESIAN_POINT('Ctrl Pts',(-7.39978217647955,0.245835647048946,
15.));
#29668=CARTESIAN_POINT('Ctrl Pts',(-7.397018590817,0.226998772493948,15.));
#29669=CARTESIAN_POINT('Ctrl Pts',(-7.39472997377155,0.208076803222566,
15.));
#29670=CARTESIAN_POINT('Ctrl Pts',(-7.39292062669322,0.189088525473043,
15.));
#29671=CARTESIAN_POINT('Ctrl Pts',(-7.39203074058723,0.179749574009065,
15.));
#29672=CARTESIAN_POINT('Ctrl Pts',(-7.39125667019278,0.170392618111359,
15.));
#29673=CARTESIAN_POINT('Ctrl Pts',(-7.39059946538832,0.161026195275006,
15.));
#29674=CARTESIAN_POINT('Ctrl Pts',(-7.38726347674367,0.113481989859994,
15.));
#29675=CARTESIAN_POINT('Ctrl Pts',(-7.38694625368064,0.0658815596571062,
15.));
#29676=CARTESIAN_POINT('Ctrl Pts',(-7.38964513362731,0.0185137802117043,
15.));
#29677=CARTESIAN_POINT('Ctrl Pts',(-7.39231343455405,-0.0283173098292195,
15.));
#29678=CARTESIAN_POINT('Ctrl Pts',(-7.39793005971206,-0.0749220643021994,
15.));
#29679=CARTESIAN_POINT('Ctrl Pts',(-7.40654190918745,-0.121012249417508,
15.));
#29680=CARTESIAN_POINT('Ctrl Pts',(-7.40892379251999,-0.133759969176599,
15.));
#29681=CARTESIAN_POINT('Ctrl Pts',(-7.41153508910055,-0.146468219675886,
15.));
#29682=CARTESIAN_POINT('Ctrl Pts',(-7.41437744335462,-0.159130611434646,
15.));
#29683=CARTESIAN_POINT('Ctrl Pts',(-7.41931615775307,-0.181132068996878,
15.));
#29684=CARTESIAN_POINT('Ctrl Pts',(-7.42495234417919,-0.202995174294252,
15.));
#29685=CARTESIAN_POINT('Ctrl Pts',(-7.43127605846836,-0.224688120790961,
15.));
#29686=CARTESIAN_POINT('Ctrl Pts',(-7.4344860198212,-0.235699611301021,
15.));
#29687=CARTESIAN_POINT('Ctrl Pts',(-7.43787316641254,-0.246667231430326,
15.));
#29688=CARTESIAN_POINT('Ctrl Pts',(-7.44143639509547,-0.257586640410256,
15.));
#29689=CARTESIAN_POINT('Ctrl Pts',(-7.4446649858989,-0.267480561499389,
15.));
#29690=CARTESIAN_POINT('Ctrl Pts',(-7.44803553776462,-0.277326794204636,
15.));
#29691=CARTESIAN_POINT('Ctrl Pts',(-7.45154507732052,-0.287118296675091,
15.));
#29692=CARTESIAN_POINT('Ctrl Pts',(-7.46731977428534,-0.331129193786157,
15.));
#29693=CARTESIAN_POINT('Ctrl Pts',(-7.48590786965047,-0.374063763344147,
15.));
#29694=CARTESIAN_POINT('Ctrl Pts',(-7.50719066652686,-0.415647384120069,
15.));
#29695=CARTESIAN_POINT('Ctrl Pts',(-7.51904302719296,-0.43880524603553,
15.));
#29696=CARTESIAN_POINT('Ctrl Pts',(-7.5317319029862,-0.461543654707363,
15.));
#29697=CARTESIAN_POINT('Ctrl Pts',(-7.54524209132987,-0.483810502964833,
15.));
#29698=CARTESIAN_POINT('Ctrl Pts',(-7.55097581847724,-0.493260558662993,
15.));
#29699=CARTESIAN_POINT('Ctrl Pts',(-7.55685694084107,-0.502624435497839,
15.));
#29700=CARTESIAN_POINT('Ctrl Pts',(-7.56287744573998,-0.511888023199772,
15.));
#29701=CARTESIAN_POINT('Ctrl Pts',(-7.58817054843871,-0.550805834751792,
15.));
#29702=CARTESIAN_POINT('Ctrl Pts',(-7.61595074867493,-0.588006977343887,
15.));
#29703=CARTESIAN_POINT('Ctrl Pts',(-7.64611669191102,-0.623204223528289,
15.));
#29704=CARTESIAN_POINT('Ctrl Pts',(-7.66532331964563,-0.645614277126032,
15.));
#29705=CARTESIAN_POINT('Ctrl Pts',(-7.68549798951779,-0.667211207796954,
15.));
#29706=CARTESIAN_POINT('Ctrl Pts',(-7.70658096099555,-0.687940818620793,
15.));
#29707=CARTESIAN_POINT('Ctrl Pts',(-7.70661869325992,-0.687936125025717,
13.8));
#29708=CARTESIAN_POINT('Ctrl Pts',(-7.67409790832043,-0.65590132663166,
13.8));
#29709=CARTESIAN_POINT('Ctrl Pts',(-7.64381311621299,-0.621806798728219,
13.8));
#29710=CARTESIAN_POINT('Ctrl Pts',(-7.61585476886247,-0.585951934642269,
13.8));
#29711=CARTESIAN_POINT('Ctrl Pts',(-7.58749800537564,-0.549586126320677,
13.8));
#29712=CARTESIAN_POINT('Ctrl Pts',(-7.56153373633204,-0.511408666095284,
13.8));
#29713=CARTESIAN_POINT('Ctrl Pts',(-7.53808668428465,-0.471686692826258,
13.8));
#29714=CARTESIAN_POINT('Ctrl Pts',(-7.51732520369006,-0.436514383081886,
13.8));
#29715=CARTESIAN_POINT('Ctrl Pts',(-7.49853744049679,-0.40013004713118,
13.8));
#29716=CARTESIAN_POINT('Ctrl Pts',(-7.48183644885479,-0.362697961579565,
13.8));
#29717=CARTESIAN_POINT('Ctrl Pts',(-7.477109485266,-0.352103374788074,13.8));
#29718=CARTESIAN_POINT('Ctrl Pts',(-7.47254853386425,-0.341421047886299,
13.8));
#29719=CARTESIAN_POINT('Ctrl Pts',(-7.46816654485215,-0.330680261275302,
13.8));
#29720=CARTESIAN_POINT('Ctrl Pts',(-7.45706638332686,-0.30347241890934,
13.8));
#29721=CARTESIAN_POINT('Ctrl Pts',(-7.44710002577023,-0.275860115753735,
13.8));
#29722=CARTESIAN_POINT('Ctrl Pts',(-7.43829488164217,-0.247911966218546,
13.8));
#29723=CARTESIAN_POINT('Ctrl Pts',(-7.42417532395293,-0.203095492583373,
13.8));
#29724=CARTESIAN_POINT('Ctrl Pts',(-7.41303896601868,-0.157416559281343,
13.8));
#29725=CARTESIAN_POINT('Ctrl Pts',(-7.40485046498018,-0.111178664922763,
13.8));
#29726=CARTESIAN_POINT('Ctrl Pts',(-7.399063774025,-0.0785030379901238,
13.8));
#29727=CARTESIAN_POINT('Ctrl Pts',(-7.39475021303378,-0.0455475244970284,
13.8));
#29728=CARTESIAN_POINT('Ctrl Pts',(-7.39191194648372,-0.0124134397669909,
13.8));
#29729=CARTESIAN_POINT('Ctrl Pts',(-7.39015335429547,0.00811646520966508,
13.8));
#29730=CARTESIAN_POINT('Ctrl Pts',(-7.38896137677175,0.0287150012886081,
13.8));
#29731=CARTESIAN_POINT('Ctrl Pts',(-7.38833895669897,0.0493584273596811,
13.8));
#29732=CARTESIAN_POINT('Ctrl Pts',(-7.38797680356068,0.0613697391144699,
13.8));
#29733=CARTESIAN_POINT('Ctrl Pts',(-7.38780768251601,0.0734006750408645,
13.8));
#29734=CARTESIAN_POINT('Ctrl Pts',(-7.38783191166033,0.0854177210780557,
13.8));
#29735=CARTESIAN_POINT('Ctrl Pts',(-7.38792937970413,0.133759418733823,
13.8));
#29736=CARTESIAN_POINT('Ctrl Pts',(-7.39114708267554,0.181957500267464,
13.8));
#29737=CARTESIAN_POINT('Ctrl Pts',(-7.39745279060964,0.229700973635331,
13.8));
#29738=CARTESIAN_POINT('Ctrl Pts',(-7.39992953931477,0.248453600156905,
13.8));
#29739=CARTESIAN_POINT('Ctrl Pts',(-7.40288323259558,0.267136279136232,
13.8));
#29740=CARTESIAN_POINT('Ctrl Pts',(-7.40631404968938,0.285730658351667,
13.8));
#29741=CARTESIAN_POINT('Ctrl Pts',(-7.41475420643096,0.33147471022025,13.8));
#29742=CARTESIAN_POINT('Ctrl Pts',(-7.42607873358428,0.376684794101564,
13.8));
#29743=CARTESIAN_POINT('Ctrl Pts',(-7.44015748288889,0.421130921718887,
13.8));
#29744=CARTESIAN_POINT('Ctrl Pts',(-7.44619773201859,0.440199780596242,
13.8));
#29745=CARTESIAN_POINT('Ctrl Pts',(-7.45274552285538,0.459127950334225,
13.8));
#29746=CARTESIAN_POINT('Ctrl Pts',(-7.45979307537158,0.477896691038924,
13.8));
#29747=CARTESIAN_POINT('Ctrl Pts',(-7.46424191712361,0.489744656284764,
13.8));
#29748=CARTESIAN_POINT('Ctrl Pts',(-7.46889207365577,0.50153379748079,13.8));
#29749=CARTESIAN_POINT('Ctrl Pts',(-7.47372950591637,0.513230703803242,
13.8));
#29750=CARTESIAN_POINT('Ctrl Pts',(-7.49246787387759,0.558540058615907,
13.8));
#29751=CARTESIAN_POINT('Ctrl Pts',(-7.51403700466946,0.602538901598153,
13.8));
#29752=CARTESIAN_POINT('Ctrl Pts',(-7.53825696201999,0.644973296328836,
13.8));
#29753=CARTESIAN_POINT('Ctrl Pts',(-7.56269793086436,0.687794912590659,
13.8));
#29754=CARTESIAN_POINT('Ctrl Pts',(-7.58983864981357,0.729024481326262,
13.8));
#29755=CARTESIAN_POINT('Ctrl Pts',(-7.61954508825485,0.768389329203374,
13.8));
#29756=CARTESIAN_POINT('Ctrl Pts',(-7.62494286994729,0.775542083499952,
13.8));
#29757=CARTESIAN_POINT('Ctrl Pts',(-7.63042548902675,0.782633214974312,
13.8));
#29758=CARTESIAN_POINT('Ctrl Pts',(-7.63599230650583,0.789661002536044,
13.8));
#29759=CARTESIAN_POINT('Ctrl Pts',(-7.65116967374115,0.8088215575708,13.8));
#29760=CARTESIAN_POINT('Ctrl Pts',(-7.66697273174487,0.827511407193791,
13.8));
#29761=CARTESIAN_POINT('Ctrl Pts',(-7.68337323824041,0.845709888164107,
13.8));
#29762=CARTESIAN_POINT('Ctrl Pts',(-7.6911253557073,0.854311864099374,13.8));
#29763=CARTESIAN_POINT('Ctrl Pts',(-7.69901099219276,0.862804028438582,
13.8));
#29764=CARTESIAN_POINT('Ctrl Pts',(-7.7070273463286,0.871184032005587,13.8));
#29765=CARTESIAN_POINT('Ctrl Pts',(-7.71445506730095,0.878948699981603,
13.8));
#29766=CARTESIAN_POINT('Ctrl Pts',(-7.72198930646464,0.886611035023255,
13.8));
#29767=CARTESIAN_POINT('Ctrl Pts',(-7.72962347583117,0.894165851015352,
13.8));
#29768=CARTESIAN_POINT('Ctrl Pts',(-7.76528151517699,0.929453242866773,
13.8));
#29769=CARTESIAN_POINT('Ctrl Pts',(-7.80314150536528,0.962423770257437,
13.8));
#29770=CARTESIAN_POINT('Ctrl Pts',(-7.84293209092609,0.992921897771992,
13.8));
#29771=CARTESIAN_POINT('Ctrl Pts',(-7.86517990438843,1.00997408844301,13.8));
#29772=CARTESIAN_POINT('Ctrl Pts',(-7.88803208111194,1.02625286763951,13.8));
#29773=CARTESIAN_POINT('Ctrl Pts',(-7.91144653285245,1.04172643812877,13.8));
#29774=CARTESIAN_POINT('Ctrl Pts',(-7.92363390847077,1.04978053300143,13.8));
#29775=CARTESIAN_POINT('Ctrl Pts',(-7.93597590810809,1.05761754617181,13.8));
#29776=CARTESIAN_POINT('Ctrl Pts',(-7.94844649246672,1.06522079436794,13.8));
#29777=CARTESIAN_POINT('Ctrl Pts',(-7.99400652040546,1.09299849830535,13.8));
#29778=CARTESIAN_POINT('Ctrl Pts',(-8.04133364966062,1.11769701342198,13.8));
#29779=CARTESIAN_POINT('Ctrl Pts',(-8.09012859132893,1.13911578403477,13.8));
#29780=CARTESIAN_POINT('Ctrl Pts',(-8.12124378281263,1.15277394461815,13.8));
#29781=CARTESIAN_POINT('Ctrl Pts',(-8.15295678898405,1.16509764664083,13.8));
#29782=CARTESIAN_POINT('Ctrl Pts',(-8.1851779246473,1.17607853534585,13.8));
#29783=CARTESIAN_POINT('Ctrl Pts',(-9.55016480120948,-1.36965928395627E-5,
14.2841069671524));
#29784=CARTESIAN_POINT('Ctrl Pts',(-9.55006211521689,0.154119214996547,
14.2770974504288));
#29785=CARTESIAN_POINT('Ctrl Pts',(-9.51567268207578,0.308296476102981,
14.2700879337053));
#29786=CARTESIAN_POINT('Ctrl Pts',(-9.44996590537973,0.447714034607548,
14.2630784169817));
#29787=CARTESIAN_POINT('Ctrl Pts',(-9.37761809754114,0.601222625946185,
14.2553604433654));
#29788=CARTESIAN_POINT('Ctrl Pts',(-9.26730249755549,0.736837192539179,
14.247642469749));
#29789=CARTESIAN_POINT('Ctrl Pts',(-9.13173789347323,0.838922113254271,
14.2399244961327));
#29790=CARTESIAN_POINT('Ctrl Pts',(-8.99617328939096,0.941007033969362,
14.2322065225163));
#29791=CARTESIAN_POINT('Ctrl Pts',(-8.83535968121208,1.00956230880655,14.2244885488999));
#29792=CARTESIAN_POINT('Ctrl Pts',(-8.66783800241227,1.03668388776098,14.2167705752836));
#29793=CARTESIAN_POINT('Ctrl Pts',(-8.50031632361246,1.06380546671541,14.2090526016672));
#29794=CARTESIAN_POINT('Ctrl Pts',(-8.32608657419173,1.04949334978708,14.2013346280508));
#29795=CARTESIAN_POINT('Ctrl Pts',(-8.16523649562096,0.995397646286945,
14.1936166544345));
#29796=CARTESIAN_POINT('Ctrl Pts',(-8.00438641705019,0.941301942786809,
14.1858986808181));
#29797=CARTESIAN_POINT('Ctrl Pts',(-7.85691600932937,0.847422652714868,
14.1781807072018));
#29798=CARTESIAN_POINT('Ctrl Pts',(-7.73982780762178,0.724583546753225,
14.1704627335854));
#29799=CARTESIAN_POINT('Ctrl Pts',(-7.62273960591418,0.601744440791583,
14.162744759969));
#29800=CARTESIAN_POINT('Ctrl Pts',(-7.5360336102198,0.44994551894024,14.1550267863527));
#29801=CARTESIAN_POINT('Ctrl Pts',(-7.48970654962093,0.286688371124695,
14.1473088127363));
#29802=CARTESIAN_POINT('Ctrl Pts',(-7.44337948902206,0.123431223309151,
14.1395908391199));
#29803=CARTESIAN_POINT('Ctrl Pts',(-7.43743136351871,-0.0512841504705941,
14.1318728655036));
#29804=CARTESIAN_POINT('Ctrl Pts',(-7.47254795990888,-0.217314020421096,
14.1241548918872));
#29805=CARTESIAN_POINT('Ctrl Pts',(-7.50766455629905,-0.383343890371597,
14.1164369182709));
#29806=CARTESIAN_POINT('Ctrl Pts',(-7.58384587458274,-0.540688256492854,
14.1087189446545));
#29807=CARTESIAN_POINT('Ctrl Pts',(-7.69230862285979,-0.671206166678132,
14.1010009710381));
#29808=CARTESIAN_POINT('Ctrl Pts',(-7.80077137113685,-0.801724076863409,
14.0932829974218));
#29809=CARTESIAN_POINT('Ctrl Pts',(-7.94151554940726,-0.905415531112706,
14.0855650238054));
#29810=CARTESIAN_POINT('Ctrl Pts',(-8.09831412167731,-0.970325476600624,
14.077847050189));
#29811=CARTESIAN_POINT('Ctrl Pts',(-8.25511269394736,-1.03523542208854,
14.0701290765727));
#29812=CARTESIAN_POINT('Ctrl Pts',(-8.42796566021704,-1.06136385881508,
14.0624111029563));
#29813=CARTESIAN_POINT('Ctrl Pts',(-8.59694401140962,-1.04569830446762,
14.05469312934));
#29814=CARTESIAN_POINT('Ctrl Pts',(-8.7659223626022,-1.03003275012016,14.0469751557236));
#29815=CARTESIAN_POINT('Ctrl Pts',(-8.93102609871766,-0.97257320469871,
14.0392571821072));
#29816=CARTESIAN_POINT('Ctrl Pts',(-9.07321966481483,-0.879944475201997,
14.0315392084909));
#29817=CARTESIAN_POINT('Ctrl Pts',(-9.215413230912,-0.787315745705285,14.0238212348745));
#29818=CARTESIAN_POINT('Ctrl Pts',(-9.33469662699088,-0.659517832133316,
14.0161032612581));
#29819=CARTESIAN_POINT('Ctrl Pts',(-9.41731711205793,-0.51128506376211,
14.0083852876418));
#29820=CARTESIAN_POINT('Ctrl Pts',(-9.49993759712498,-0.363052295390903,
14.0006673140254));
#29821=CARTESIAN_POINT('Ctrl Pts',(-9.54589517118021,-0.194384672220457,
13.9929493404091));
#29822=CARTESIAN_POINT('Ctrl Pts',(-9.54989120883354,-0.0247288136166145,
13.9852313667927));
#29823=CARTESIAN_POINT('Ctrl Pts',(-9.55008526423043,-0.0164899936069937,
13.9848565669126));
#29824=CARTESIAN_POINT('Ctrl Pts',(-9.55018036327262,-0.00824884307793844,
13.9844817670325));
#29825=CARTESIAN_POINT('Ctrl Pts',(-9.55017700723911,-7.61513114500012E-6,
13.9841069671524));
#29826=CARTESIAN_POINT('Ctrl Pts',(-8.81478889550439,1.17604951161383,13.8));
#29827=CARTESIAN_POINT('Ctrl Pts',(-9.00489125583826,1.12516550422186,13.8077179736164));
#29828=CARTESIAN_POINT('Ctrl Pts',(-9.35978714971093,0.929517388355175,
13.8231539208491));
#29829=CARTESIAN_POINT('Ctrl Pts',(-9.69399194673282,0.421519158642242,
13.8463078416982));
#29830=CARTESIAN_POINT('Ctrl Pts',(-9.75281425601952,-0.18363315341468,
13.8694617625473));
#29831=CARTESIAN_POINT('Ctrl Pts',(-9.52277717161101,-0.746471281904888,
13.8926156833963));
#29832=CARTESIAN_POINT('Ctrl Pts',(-9.05688631633702,-1.13717009764717,
13.9157696042454));
#29833=CARTESIAN_POINT('Ctrl Pts',(-8.46258916536876,-1.26565565606363,
13.9389235250945));
#29834=CARTESIAN_POINT('Ctrl Pts',(-7.87691591618916,-1.10229229667761,
13.9620774459436));
#29835=CARTESIAN_POINT('Ctrl Pts',(-7.43492027566404,-0.684753533801549,
13.9852313667927));
#29836=CARTESIAN_POINT('Ctrl Pts',(-7.23851986425691,-0.109317520883414,
14.0083852876418));
#29837=CARTESIAN_POINT('Ctrl Pts',(-7.33300329226471,0.491325669494413,
14.0315392084909));
#29838=CARTESIAN_POINT('Ctrl Pts',(-7.6965833349978,0.978674626363476,14.05469312934));
#29839=CARTESIAN_POINT('Ctrl Pts',(-8.24542256676704,1.24035181775585,14.077847050189));
#29840=CARTESIAN_POINT('Ctrl Pts',(-8.8529645573119,1.21601741100899,14.1010009710381));
#29841=CARTESIAN_POINT('Ctrl Pts',(-9.37911677604257,0.911282619288843,
14.1241548918872));
#29842=CARTESIAN_POINT('Ctrl Pts',(-9.70255423368964,0.396415983899717,
14.1473088127363));
#29843=CARTESIAN_POINT('Ctrl Pts',(-9.74869578230927,-0.209859863166589,
14.1704627335854));
#29844=CARTESIAN_POINT('Ctrl Pts',(-9.50690167961977,-0.767744309864743,
14.1936166544345));
#29845=CARTESIAN_POINT('Ctrl Pts',(-9.03292701443594,-1.14859527930365,
14.2167705752836));
#29846=CARTESIAN_POINT('Ctrl Pts',(-8.43606518260107,-1.26459268432005,
14.2399244961327));
#29847=CARTESIAN_POINT('Ctrl Pts',(-7.85394602357466,-1.08898878677709,
14.2630784169817));
#29848=CARTESIAN_POINT('Ctrl Pts',(-7.4207998764838,-0.662275933111461,
14.2862323378308));
#29849=CARTESIAN_POINT('Ctrl Pts',(-7.23650552633111,-0.0828494609134307,
14.3093862586799));
#29850=CARTESIAN_POINT('Ctrl Pts',(-7.3435592434188,0.515681194822054,14.332540179529));
#29851=CARTESIAN_POINT('Ctrl Pts',(-7.71727560632613,0.995301382354801,
14.3556941003781));
#29852=CARTESIAN_POINT('Ctrl Pts',(-8.27147969121155,1.24541590910158,14.3788480212272));
#29853=CARTESIAN_POINT('Ctrl Pts',(-8.87837807091352,1.20835108872504,14.4020019420763));
#29854=CARTESIAN_POINT('Ctrl Pts',(-9.39802658767663,0.892653665201231,
14.4251558629254));
#29855=CARTESIAN_POINT('Ctrl Pts',(-9.71059995206503,0.371120026718582,
14.4483097837744));
#29856=CARTESIAN_POINT('Ctrl Pts',(-9.74402214990757,-0.235989848744997,
14.4714637046235));
#29857=CARTESIAN_POINT('Ctrl Pts',(-9.49058638632123,-0.788683034815797,
14.4946176254726));
#29858=CARTESIAN_POINT('Ctrl Pts',(-9.00873218868954,-1.159514501144,14.5177715463217));
#29859=CARTESIAN_POINT('Ctrl Pts',(-8.40956988800579,-1.26297454963044,
14.5409254671708));
#29860=CARTESIAN_POINT('Ctrl Pts',(-7.8312597864405,-1.07520641969046,14.5640793880199));
#29861=CARTESIAN_POINT('Ctrl Pts',(-7.40715389611314,-0.639507397443362,
14.587233308869));
#29862=CARTESIAN_POINT('Ctrl Pts',(-7.23504641717748,-0.0563449330507459,
14.6103872297181));
#29863=CARTESIAN_POINT('Ctrl Pts',(-7.35462346018219,0.539810059387775,
14.6335411505671));
#29864=CARTESIAN_POINT('Ctrl Pts',(-7.73831186108132,1.01149073013163,14.6566950714162));
#29865=CARTESIAN_POINT('Ctrl Pts',(-8.29763725271243,1.24993265293153,14.6798489922653));
#29866=CARTESIAN_POINT('Ctrl Pts',(-8.9036252902427,1.20015371633275,14.7030029131144));
#29867=CARTESIAN_POINT('Ctrl Pts',(-9.4165417311248,0.873632402118881,14.7261568339635));
#29868=CARTESIAN_POINT('Ctrl Pts',(-9.71811362884852,0.345660967523886,
14.7493107548126));
#29869=CARTESIAN_POINT('Ctrl Pts',(-9.73880178866775,-0.262016118838121,
14.7724646756617));
#29870=CARTESIAN_POINT('Ctrl Pts',(-9.47383574401748,-0.809275148678942,
14.7956185965108));
#29871=CARTESIAN_POINT('Ctrl Pts',(-8.98431378427829,-1.16992412560805,
14.8187725173598));
#29872=CARTESIAN_POINT('Ctrl Pts',(-8.38311433260251,-1.26080137319404,
14.8419264382089));
#29873=CARTESIAN_POINT('Ctrl Pts',(-7.80886745824715,-1.06095147820218,
14.865080359058));
#29874=CARTESIAN_POINT('Ctrl Pts',(-7.39398818892938,-0.616457887465797,
14.8882342799071));
#29875=CARTESIAN_POINT('Ctrl Pts',(-7.23414327069309,-0.0298154676920097,
14.9113882007562));
#29876=CARTESIAN_POINT('Ctrl Pts',(-7.36619097191447,0.563701313325544,
14.9345421216053));
#29877=CARTESIAN_POINT('Ctrl Pts',(-7.75968301484676,1.02723637580027,14.9576960424544));
#29878=CARTESIAN_POINT('Ctrl Pts',(-8.32388331973028,1.25389836718814,14.9808499633034));
#29879=CARTESIAN_POINT('Ctrl Pts',(-8.9286956299142,1.19143299197639,15.0040038841525));
#29880=CARTESIAN_POINT('Ctrl Pts',(-9.43465130660384,0.85421989568406,15.0271578050016));
#29881=CARTESIAN_POINT('Ctrl Pts',(-9.72509144430676,0.320072059154916,
15.0503117258507));
#29882=CARTESIAN_POINT('Ctrl Pts',(-9.73301282108904,-0.287951213042609,
15.0734656466998));
#29883=CARTESIAN_POINT('Ctrl Pts',(-9.54874216054247,-0.648885562186042,
15.0889015939325));
#29884=CARTESIAN_POINT('Ctrl Pts',(-9.4198191333118,-0.797569598526378,
15.0966195675489));
#29885=CARTESIAN_POINT('Ctrl Pts',(-8.80036532666169,1.12216314098435,13.7677934774837));
#29886=CARTESIAN_POINT('Ctrl Pts',(-8.98175723208245,1.07361062937922,13.7755114511001));
#29887=CARTESIAN_POINT('Ctrl Pts',(-9.32039186188141,0.886927073916187,
13.7909473983328));
#29888=CARTESIAN_POINT('Ctrl Pts',(-9.639283457052,0.402205228926093,13.8141013191819));
#29889=CARTESIAN_POINT('Ctrl Pts',(-9.69541053903049,-0.175219116363481,
13.837255240031));
#29890=CARTESIAN_POINT('Ctrl Pts',(-9.47591371118989,-0.712268106134006,
13.8604091608801));
#29891=CARTESIAN_POINT('Ctrl Pts',(-9.03136988854697,-1.08506517455896,
13.8835630817291));
#29892=CARTESIAN_POINT('Ctrl Pts',(-8.46430332287709,-1.20766354850487,
13.9067170025782));
#29893=CARTESIAN_POINT('Ctrl Pts',(-7.90546551341444,-1.05178546796487,
13.9298709234273));
#29894=CARTESIAN_POINT('Ctrl Pts',(-7.48372203120982,-0.653378253808753,
13.9530248442764));
#29895=CARTESIAN_POINT('Ctrl Pts',(-7.29632065024857,-0.104308612339644,
13.9761787651255));
#29896=CARTESIAN_POINT('Ctrl Pts',(-7.3864748650985,0.46881321839036,13.9993326859746));
#29897=CARTESIAN_POINT('Ctrl Pts',(-7.7333957376668,0.933831936390738,14.0224866068237));
#29898=CARTESIAN_POINT('Ctrl Pts',(-8.25708725756928,1.18351912737802,14.0456405276728));
#29899=CARTESIAN_POINT('Ctrl Pts',(-8.83679178672141,1.16029971863768,14.0687944485218));
#29900=CARTESIAN_POINT('Ctrl Pts',(-9.33883580831748,0.869527818588475,
14.0919483693709));
#29901=CARTESIAN_POINT('Ctrl Pts',(-9.64745342160757,0.378252276997143,
14.11510229022));
#29902=CARTESIAN_POINT('Ctrl Pts',(-9.69148077302225,-0.200244123135943,
14.1382562110691));
#29903=CARTESIAN_POINT('Ctrl Pts',(-9.460765631299,-0.73256640789591,14.1614101319182));
#29904=CARTESIAN_POINT('Ctrl Pts',(-9.00850839741789,-1.0959668565097,14.1845640527673));
#29905=CARTESIAN_POINT('Ctrl Pts',(-8.43899466408332,-1.20664928192954,
14.2077179736164));
#29906=CARTESIAN_POINT('Ctrl Pts',(-7.88354809702183,-1.03909152242205,
14.2308718944655));
#29907=CARTESIAN_POINT('Ctrl Pts',(-7.47024862610266,-0.631930572615834,
14.2540258153145));
#29908=CARTESIAN_POINT('Ctrl Pts',(-7.29439860891314,-0.0790533139713622,
14.2771797361636));
#29909=CARTESIAN_POINT('Ctrl Pts',(-7.39654714452737,0.49205277806203,14.3003336570127));
#29910=CARTESIAN_POINT('Ctrl Pts',(-7.75313989295838,0.949696857504478,
14.3234875778618));
#29911=CARTESIAN_POINT('Ctrl Pts',(-8.28195044940169,1.18835118299697,14.3466414987109));
#29912=CARTESIAN_POINT('Ctrl Pts',(-8.86104085784046,1.15298466581975,14.36979541956));
#29913=CARTESIAN_POINT('Ctrl Pts',(-9.3568791758876,0.851752439724092,14.3929493404091));
#29914=CARTESIAN_POINT('Ctrl Pts',(-9.65513048665835,0.354115375885186,
14.4161032612581));
#29915=CARTESIAN_POINT('Ctrl Pts',(-9.68702128559088,-0.225176837618606,
14.4392571821072));
#29916=CARTESIAN_POINT('Ctrl Pts',(-9.4451979017152,-0.752545724350912,
14.4624111029563));
#29917=CARTESIAN_POINT('Ctrl Pts',(-8.98542217410244,-1.10638576162932,
14.4855650238054));
#29918=CARTESIAN_POINT('Ctrl Pts',(-8.41371337897523,-1.20510528987148,
14.5087189446545));
#29919=CARTESIAN_POINT('Ctrl Pts',(-7.86190133906803,-1.02594066084063,
14.5318728655036));
#29920=CARTESIAN_POINT('Ctrl Pts',(-7.45722790202316,-0.610205287031669,
14.5550267863527));
#29921=CARTESIAN_POINT('Ctrl Pts',(-7.29300635587047,-0.0537632186624639,
14.5781807072018));
#29922=CARTESIAN_POINT('Ctrl Pts',(-7.40710440092952,0.515076062525879,
14.6013346280508));
#29923=CARTESIAN_POINT('Ctrl Pts',(-7.77321227041997,0.965144412367029,
14.6244885488999));
#29924=CARTESIAN_POINT('Ctrl Pts',(-8.30690947628316,1.19266097046186,14.647642469749));
#29925=CARTESIAN_POINT('Ctrl Pts',(-8.88513125425981,1.14516289551101,14.6707963905981));
#29926=CARTESIAN_POINT('Ctrl Pts',(-9.37454595889494,0.833602727390392,
14.6939503114472));
#29927=CARTESIAN_POINT('Ctrl Pts',(-9.66229988816436,0.329822846063696,
14.7171042322963));
#29928=CARTESIAN_POINT('Ctrl Pts',(-9.68204012033543,-0.250010588840295,
14.7402581531454));
#29929=CARTESIAN_POINT('Ctrl Pts',(-9.4292147707369,-0.772194311373804,
14.7634120739945));
#29930=CARTESIAN_POINT('Ctrl Pts',(-8.96212261645511,-1.11631841902995,
14.7865659948435));
#29931=CARTESIAN_POINT('Ctrl Pts',(-8.38847001221673,-1.20303168797658,
14.8097199156926));
#29932=CARTESIAN_POINT('Ctrl Pts',(-7.84053502320186,-1.01233887812903,
14.8328738365417));
#29933=CARTESIAN_POINT('Ctrl Pts',(-7.44466544510217,-0.588211901328816,
14.8560277573908));
#29934=CARTESIAN_POINT('Ctrl Pts',(-7.29214459139059,-0.0284493284889608,
14.8791816782399));
#29935=CARTESIAN_POINT('Ctrl Pts',(-7.41814189141838,0.537872623636706,
14.902335599089));
#29936=CARTESIAN_POINT('Ctrl Pts',(-7.79360420188124,0.980168595469752,
14.9254895199381));
#29937=CARTESIAN_POINT('Ctrl Pts',(-8.33195295337524,1.19644497642632,14.9486434407871));
#29938=CARTESIAN_POINT('Ctrl Pts',(-8.9090528756146,1.13684175312818,14.9717973616362));
#29939=CARTESIAN_POINT('Ctrl Pts',(-9.39182575698232,0.815079698402111,
14.9949512824853));
#29940=CARTESIAN_POINT('Ctrl Pts',(-9.6689579814117,0.30540641673303,15.0181052033344));
#29941=CARTESIAN_POINT('Ctrl Pts',(-9.67651640217813,-0.274757341835666,
15.0412591241835));
#29942=CARTESIAN_POINT('Ctrl Pts',(-9.50068898914137,-0.619153746004177,
15.0566950714162));
#29943=CARTESIAN_POINT('Ctrl Pts',(-9.37767319112123,-0.761025107359488,
15.0644130450326));
#29944=CARTESIAN_POINT('Ctrl Pts',(-8.78594175781898,1.06827677035487,13.7355869549674));
#29945=CARTESIAN_POINT('Ctrl Pts',(-8.95862320832664,1.02205575453658,13.7433049285838));
#29946=CARTESIAN_POINT('Ctrl Pts',(-9.2809965740519,0.844336759477199,13.7587408758165));
#29947=CARTESIAN_POINT('Ctrl Pts',(-9.58457496737118,0.382891299209943,
13.7818947966656));
#29948=CARTESIAN_POINT('Ctrl Pts',(-9.63800682204146,-0.166805079312282,
13.8050487175147));
#29949=CARTESIAN_POINT('Ctrl Pts',(-9.42905025076876,-0.678064930363123,
13.8282026383638));
#29950=CARTESIAN_POINT('Ctrl Pts',(-9.00585346075692,-1.03296025147074,
13.8513565592128));
#29951=CARTESIAN_POINT('Ctrl Pts',(-8.46601748038542,-1.1496714409461,13.8745104800619));
#29952=CARTESIAN_POINT('Ctrl Pts',(-7.93401511063972,-1.00127863925212,
13.897664400911));
#29953=CARTESIAN_POINT('Ctrl Pts',(-7.5325237867556,-0.622002973815956,
13.9208183217601));
#29954=CARTESIAN_POINT('Ctrl Pts',(-7.35412143624022,-0.099299703795874,
13.9439722426092));
#29955=CARTESIAN_POINT('Ctrl Pts',(-7.4399464379323,0.446300767286306,13.9671261634583));
#29956=CARTESIAN_POINT('Ctrl Pts',(-7.7702081403358,0.888989246418001,13.9902800843074));
#29957=CARTESIAN_POINT('Ctrl Pts',(-8.26875194837151,1.1266864370002,14.0134340051564));
#29958=CARTESIAN_POINT('Ctrl Pts',(-8.82061901613093,1.10458202626637,14.0365879260055));
#29959=CARTESIAN_POINT('Ctrl Pts',(-9.2985548405924,0.827773017888108,14.0597418468546));
#29960=CARTESIAN_POINT('Ctrl Pts',(-9.59235260952549,0.360088570094568,
14.0828957677037));
#29961=CARTESIAN_POINT('Ctrl Pts',(-9.63426576373522,-0.190628383105298,
14.1060496885528));
#29962=CARTESIAN_POINT('Ctrl Pts',(-9.41462958297823,-0.697388505927078,
14.1292036094019));
#29963=CARTESIAN_POINT('Ctrl Pts',(-8.98408978039985,-1.04333843371576,
14.152357530251));
#29964=CARTESIAN_POINT('Ctrl Pts',(-8.44192414556558,-1.14870587953904,
14.1755114511001));
#29965=CARTESIAN_POINT('Ctrl Pts',(-7.913150170469,-0.989194258067005,14.1986653719492));
#29966=CARTESIAN_POINT('Ctrl Pts',(-7.51969737572152,-0.601585212120206,
14.2218192927982));
#29967=CARTESIAN_POINT('Ctrl Pts',(-7.35229169149517,-0.0752571670292948,
14.2449732136473));
#29968=CARTESIAN_POINT('Ctrl Pts',(-7.44953504563593,0.468424361302008,
14.2681271344964));
#29969=CARTESIAN_POINT('Ctrl Pts',(-7.78900417959064,0.904092332654155,
14.2912810553455));
#29970=CARTESIAN_POINT('Ctrl Pts',(-8.29242120759183,1.13128645689237,14.3144349761946));
#29971=CARTESIAN_POINT('Ctrl Pts',(-8.8437036447674,1.09761824291446,14.3375888970437));
#29972=CARTESIAN_POINT('Ctrl Pts',(-9.31573176409856,0.810851214246954,
14.3607428178928));
#29973=CARTESIAN_POINT('Ctrl Pts',(-9.59966102125167,0.337110725051789,
14.3838967387418));
#29974=CARTESIAN_POINT('Ctrl Pts',(-9.6300204212742,-0.214363826492215,
14.4070506595909));
#29975=CARTESIAN_POINT('Ctrl Pts',(-9.39980941710916,-0.716408413886026,
14.43020458044));
#29976=CARTESIAN_POINT('Ctrl Pts',(-8.96211215951534,-1.05325702211464,
14.4533585012891));
#29977=CARTESIAN_POINT('Ctrl Pts',(-8.41785686994467,-1.14723603011252,
14.4765124221382));
#29978=CARTESIAN_POINT('Ctrl Pts',(-7.89254289169556,-0.976674901990792,
14.4996663429873));
#29979=CARTESIAN_POINT('Ctrl Pts',(-7.50730190793318,-0.580903176619976,
14.5228202638364));
#29980=CARTESIAN_POINT('Ctrl Pts',(-7.35096629456346,-0.0511815042741817,
14.5459741846855));
#29981=CARTESIAN_POINT('Ctrl Pts',(-7.45958534167685,0.490342065663984,
14.5691281055345));
#29982=CARTESIAN_POINT('Ctrl Pts',(-7.80811267975863,0.918798094602432,
14.5922820263836));
#29983=CARTESIAN_POINT('Ctrl Pts',(-8.3161816998539,1.1353892879922,14.6154359472327));
#29984=CARTESIAN_POINT('Ctrl Pts',(-8.86663721827691,1.09017207468927,14.6385898680818));
#29985=CARTESIAN_POINT('Ctrl Pts',(-9.33255018666507,0.793573052661904,
14.6617437889309));
#29986=CARTESIAN_POINT('Ctrl Pts',(-9.6064861474802,0.313984724603508,14.68489770978));
#29987=CARTESIAN_POINT('Ctrl Pts',(-9.62527845200311,-0.238005058842469,
14.7080516306291));
#29988=CARTESIAN_POINT('Ctrl Pts',(-9.38459379745632,-0.735113474068666,
14.7312055514782));
#29989=CARTESIAN_POINT('Ctrl Pts',(-8.93993144863193,-1.06271271245186,
14.7543594723273));
#29990=CARTESIAN_POINT('Ctrl Pts',(-8.39382569183094,-1.14526200275911,
14.7775133931763));
#29991=CARTESIAN_POINT('Ctrl Pts',(-7.87220258815657,-0.963726278055894,
14.8006673140254));
#29992=CARTESIAN_POINT('Ctrl Pts',(-7.49534270127495,-0.559965915191835,
14.8238212348745));
#29993=CARTESIAN_POINT('Ctrl Pts',(-7.35014591208809,-0.0270831892859103,
14.8469751557236));
#29994=CARTESIAN_POINT('Ctrl Pts',(-7.47009281092229,0.512043933947867,
14.8701290765727));
#29995=CARTESIAN_POINT('Ctrl Pts',(-7.82752538891573,0.933100815139231,
14.8932829974218));
#29996=CARTESIAN_POINT('Ctrl Pts',(-8.34002258702019,1.1389915856645,14.9164369182709));
#29997=CARTESIAN_POINT('Ctrl Pts',(-8.889410121315,1.08225051427998,14.9395908391199));
#29998=CARTESIAN_POINT('Ctrl Pts',(-9.3490002073608,0.775939501120161,14.962744759969));
#29999=CARTESIAN_POINT('Ctrl Pts',(-9.61282451851665,0.290740774311144,
14.9858986808181));
#30000=CARTESIAN_POINT('Ctrl Pts',(-9.62001998326722,-0.261563470628722,
15.0090526016672));
#30001=CARTESIAN_POINT('Ctrl Pts',(-9.45263581774028,-0.589421929822312,
15.0244885488999));
#30002=CARTESIAN_POINT('Ctrl Pts',(-9.33552724893066,-0.724480616192598,
15.0322065225163));
#30003=CARTESIAN_POINT('Ctrl Pts',(-8.77151818897627,1.01439039972539,13.7033804324511));
#30004=CARTESIAN_POINT('Ctrl Pts',(-8.93548918457083,0.970500879693933,
13.7110984060675));
#30005=CARTESIAN_POINT('Ctrl Pts',(-9.24160128622238,0.80174644503821,13.7265343533002));
#30006=CARTESIAN_POINT('Ctrl Pts',(-9.52986647769036,0.363577369493793,
13.7496882741493));
#30007=CARTESIAN_POINT('Ctrl Pts',(-9.58060310505244,-0.158391042261083,
13.7728421949984));
#30008=CARTESIAN_POINT('Ctrl Pts',(-9.38218679034763,-0.64386175459224,
13.7959961158475));
#30009=CARTESIAN_POINT('Ctrl Pts',(-8.98033703296686,-0.980855328382519,
13.8191500366965));
#30010=CARTESIAN_POINT('Ctrl Pts',(-8.46773163789374,-1.09167933338734,
13.8423039575456));
#30011=CARTESIAN_POINT('Ctrl Pts',(-7.962564707865,-0.950771810539374,13.8654578783947));
#30012=CARTESIAN_POINT('Ctrl Pts',(-7.58132554230138,-0.59062769382316,
13.8886117992438));
#30013=CARTESIAN_POINT('Ctrl Pts',(-7.41192222223187,-0.0942907952521036,
13.9117657200929));
#30014=CARTESIAN_POINT('Ctrl Pts',(-7.49341801076609,0.423788316182253,
13.934919640942));
#30015=CARTESIAN_POINT('Ctrl Pts',(-7.8070205430048,0.844146556445263,13.9580735617911));
#30016=CARTESIAN_POINT('Ctrl Pts',(-8.28041663917374,1.06985374662238,13.9812274826402));
#30017=CARTESIAN_POINT('Ctrl Pts',(-8.80444624554045,1.04886433389506,14.0043814034893));
#30018=CARTESIAN_POINT('Ctrl Pts',(-9.25827387286731,0.78601821718774,14.0275353243383));
#30019=CARTESIAN_POINT('Ctrl Pts',(-9.53725179744342,0.341924863191994,
14.0506892451874));
#30020=CARTESIAN_POINT('Ctrl Pts',(-9.5770507544482,-0.181012643074652,
14.0738431660365));
#30021=CARTESIAN_POINT('Ctrl Pts',(-9.36849353465746,-0.662210603958245,
14.0969970868856));
#30022=CARTESIAN_POINT('Ctrl Pts',(-8.95967116338181,-0.990710010921813,
14.1201510077347));
#30023=CARTESIAN_POINT('Ctrl Pts',(-8.44485362704783,-1.09076247714853,
14.1433049285838));
#30024=CARTESIAN_POINT('Ctrl Pts',(-7.94275224391618,-0.93929699371196,
14.1664588494329));
#30025=CARTESIAN_POINT('Ctrl Pts',(-7.56914612534038,-0.57123985162458,
14.1896127702819));
#30026=CARTESIAN_POINT('Ctrl Pts',(-7.4101847740772,-0.0714610200872263,
14.212766691131));
#30027=CARTESIAN_POINT('Ctrl Pts',(-7.50252294674449,0.444795944541984,
14.2359206119801));
#30028=CARTESIAN_POINT('Ctrl Pts',(-7.8248684662229,0.858487807803833,14.2590745328292));
#30029=CARTESIAN_POINT('Ctrl Pts',(-8.30289196578197,1.07422173078777,14.2822284536783));
#30030=CARTESIAN_POINT('Ctrl Pts',(-8.82636643169434,1.04225182000917,14.3053823745274));
#30031=CARTESIAN_POINT('Ctrl Pts',(-9.27458435230953,0.769949988769815,
14.3285362953765));
#30032=CARTESIAN_POINT('Ctrl Pts',(-9.54419155584499,0.320106074218393,
14.3516902162256));
#30033=CARTESIAN_POINT('Ctrl Pts',(-9.57301955695752,-0.203550815365823,
14.3748441370746));
#30034=CARTESIAN_POINT('Ctrl Pts',(-9.35442093250312,-0.680271103421141,
14.3979980579237));
#30035=CARTESIAN_POINT('Ctrl Pts',(-8.93880214492824,-1.00012828259996,
14.4211519787728));
#30036=CARTESIAN_POINT('Ctrl Pts',(-8.42200036091411,-1.08936677035355,
14.4443058996219));
#30037=CARTESIAN_POINT('Ctrl Pts',(-7.9231844443231,-0.927409143140955,
14.467459820471));
#30038=CARTESIAN_POINT('Ctrl Pts',(-7.5573759138432,-0.551601066208283,
14.4906137413201));
#30039=CARTESIAN_POINT('Ctrl Pts',(-7.40892623325645,-0.0485997898858995,
14.5137676621692));
#30040=CARTESIAN_POINT('Ctrl Pts',(-7.51206628242418,0.465608068802088,
14.5369215830183));
#30041=CARTESIAN_POINT('Ctrl Pts',(-7.84301308909729,0.872451776837834,
14.5600755038673));
#30042=CARTESIAN_POINT('Ctrl Pts',(-8.32545392342464,1.07811760552253,14.5832294247164));
#30043=CARTESIAN_POINT('Ctrl Pts',(-8.84814318229402,1.03518125386753,14.6063833455655));
#30044=CARTESIAN_POINT('Ctrl Pts',(-9.29055441443522,0.753543377933415,
14.6295372664146));
#30045=CARTESIAN_POINT('Ctrl Pts',(-9.55067240679603,0.298146603143318,
14.6526911872637));
#30046=CARTESIAN_POINT('Ctrl Pts',(-9.56851678367079,-0.225999528844643,
14.6758451081128));
#30047=CARTESIAN_POINT('Ctrl Pts',(-9.33997282417574,-0.698032636763528,
14.6989990289619));
#30048=CARTESIAN_POINT('Ctrl Pts',(-8.91774028080876,-1.00910700587376,
14.722152949811));
#30049=CARTESIAN_POINT('Ctrl Pts',(-8.39918137144515,-1.08749231754164,
14.74530687066));
#30050=CARTESIAN_POINT('Ctrl Pts',(-7.90387015311128,-0.915113677982754,
14.7684607915091));
#30051=CARTESIAN_POINT('Ctrl Pts',(-7.54601995744774,-0.531719929054855,
14.7916147123582));
#30052=CARTESIAN_POINT('Ctrl Pts',(-7.40814723278559,-0.0257170500828612,
14.8147686332073));
#30053=CARTESIAN_POINT('Ctrl Pts',(-7.52204373042621,0.486215244259028,
14.8379225540564));
#30054=CARTESIAN_POINT('Ctrl Pts',(-7.86144657595021,0.886033034808711,
14.8610764749055));
#30055=CARTESIAN_POINT('Ctrl Pts',(-8.34809222066514,1.08153819490268,14.8842303957546));
#30056=CARTESIAN_POINT('Ctrl Pts',(-8.8697673670154,1.02765927543177,14.9073843166036));
#30057=CARTESIAN_POINT('Ctrl Pts',(-9.30617465773928,0.736799303838212,
14.9305382374527));
#30058=CARTESIAN_POINT('Ctrl Pts',(-9.5566910556216,0.276075131889258,14.9536921583018));
#30059=CARTESIAN_POINT('Ctrl Pts',(-9.56352356435632,-0.248369599421778,
14.9768460791509));
#30060=CARTESIAN_POINT('Ctrl Pts',(-9.40458264633919,-0.559690113640447,
14.9922820263836));
#30061=CARTESIAN_POINT('Ctrl Pts',(-9.29338130674009,-0.687936125025709,
15.));
#30062=CARTESIAN_POINT('Ctrl Pts',(-9.29338130674009,-0.687936125025709,
15.));
#30063=CARTESIAN_POINT('Ctrl Pts',(-9.3259020578849,-0.655901359921301,
15.));
#30064=CARTESIAN_POINT('Ctrl Pts',(-9.35618681437,-0.62180686309643,15.));
#30065=CARTESIAN_POINT('Ctrl Pts',(-9.38414512772406,-0.585952030068796,
15.));
#30066=CARTESIAN_POINT('Ctrl Pts',(-9.41250187315505,-0.54958623218394,
15.));
#30067=CARTESIAN_POINT('Ctrl Pts',(-9.43846612303508,-0.511408780275333,
15.));
#30068=CARTESIAN_POINT('Ctrl Pts',(-9.46191315816531,-0.471686815958835,
15.));
#30069=CARTESIAN_POINT('Ctrl Pts',(-9.48267465073316,-0.436514468480486,
15.));
#30070=CARTESIAN_POINT('Ctrl Pts',(-9.50146242253628,-0.400130092146184,
15.));
#30071=CARTESIAN_POINT('Ctrl Pts',(-9.51816342133453,-0.362697966110186,
15.));
#30072=CARTESIAN_POINT('Ctrl Pts',(-9.52289039443137,-0.352103351089404,
15.));
#30073=CARTESIAN_POINT('Ctrl Pts',(-9.5274513547165,-0.341420995627983,
15.));
#30074=CARTESIAN_POINT('Ctrl Pts',(-9.5318333519652,-0.330680180343462,
15.));
#30075=CARTESIAN_POINT('Ctrl Pts',(-9.5429335098473,-0.303472325414772,
15.));
#30076=CARTESIAN_POINT('Ctrl Pts',(-9.55289986461919,-0.27586001076394,
15.));
#30077=CARTESIAN_POINT('Ctrl Pts',(-9.56170500757217,-0.247911851598931,
15.));
#30078=CARTESIAN_POINT('Ctrl Pts',(-9.57582456759079,-0.203095349147118,
15.));
#30079=CARTESIAN_POINT('Ctrl Pts',(-9.58696093020466,-0.157416391299935,
15.));
#30080=CARTESIAN_POINT('Ctrl Pts',(-9.59514943628876,-0.111178475189023,
15.));
#30081=CARTESIAN_POINT('Ctrl Pts',(-9.60093612680025,-0.0785028555238702,
15.));
#30082=CARTESIAN_POINT('Ctrl Pts',(-9.60524968957201,-0.0455473510823616,
15.));
#30083=CARTESIAN_POINT('Ctrl Pts',(-9.60808795943142,-0.0124132764720893,
15.));
#30084=CARTESIAN_POINT('Ctrl Pts',(-9.60984655705952,0.00811666180204036,
15.));
#30085=CARTESIAN_POINT('Ctrl Pts',(-9.61103853842703,0.0287152310324904,
15.));
#30086=CARTESIAN_POINT('Ctrl Pts',(-9.61166096056637,0.0493586901403063,
15.));
#30087=CARTESIAN_POINT('Ctrl Pts',(-9.61202311273082,0.0613699489391692,
15.));
#30088=CARTESIAN_POINT('Ctrl Pts',(-9.61219223451897,0.0734008315968733,
15.));
#30089=CARTESIAN_POINT('Ctrl Pts',(-9.61216800780618,0.0854178244046445,
15.));
#30090=CARTESIAN_POINT('Ctrl Pts',(-9.61207054909412,0.133759531018345,
15.));
#30091=CARTESIAN_POINT('Ctrl Pts',(-9.60885285388807,0.181957620798743,
15.));
#30092=CARTESIAN_POINT('Ctrl Pts',(-9.60254715011237,0.22970110335093,15.));
#30093=CARTESIAN_POINT('Ctrl Pts',(-9.60007040651486,0.248453707174439,
15.));
#30094=CARTESIAN_POINT('Ctrl Pts',(-9.59711671912308,0.267136363796024,
15.));
#30095=CARTESIAN_POINT('Ctrl Pts',(-9.59368590857673,0.285730721169551,
15.));
#30096=CARTESIAN_POINT('Ctrl Pts',(-9.58524575907286,0.331474767376859,
15.));
#30097=CARTESIAN_POINT('Ctrl Pts',(-9.57392123707722,0.37668484759268,15.));
#30098=CARTESIAN_POINT('Ctrl Pts',(-9.55984249148786,0.421130972866353,
15.));
#30099=CARTESIAN_POINT('Ctrl Pts',(-9.55380224394171,0.440199830771102,
15.));
#30100=CARTESIAN_POINT('Ctrl Pts',(-9.54725445442082,0.459127999779685,
15.));
#30101=CARTESIAN_POINT('Ctrl Pts',(-9.54020690300201,0.47789673994602,15.));
#30102=CARTESIAN_POINT('Ctrl Pts',(-9.53575806190591,0.489744704950029,
15.));
#30103=CARTESIAN_POINT('Ctrl Pts',(-9.53110790593948,0.501533845979217,
15.));
#30104=CARTESIAN_POINT('Ctrl Pts',(-9.52627047416585,0.513230752196449,
15.));
#30105=CARTESIAN_POINT('Ctrl Pts',(-9.50753211141022,0.558540098575664,
15.));
#30106=CARTESIAN_POINT('Ctrl Pts',(-9.48596298565104,0.60253893451057,15.));
#30107=CARTESIAN_POINT('Ctrl Pts',(-9.46174303380365,0.644973322939031,
15.));
#30108=CARTESIAN_POINT('Ctrl Pts',(-9.43730206706482,0.687794938881859,
15.));
#30109=CARTESIAN_POINT('Ctrl Pts',(-9.410161349938,0.729024507609743,15.));
#30110=CARTESIAN_POINT('Ctrl Pts',(-9.38045491375756,0.768389355049031,
15.));
#30111=CARTESIAN_POINT('Ctrl Pts',(-9.37505712673739,0.77554211687035,15.));
#30112=CARTESIAN_POINT('Ctrl Pts',(-9.36957450216427,0.782633255724265,
15.));
#30113=CARTESIAN_POINT('Ctrl Pts',(-9.36400767903199,0.789661050510416,
15.));
#30114=CARTESIAN_POINT('Ctrl Pts',(-9.34883031194736,0.808821605593667,
15.));
#30115=CARTESIAN_POINT('Ctrl Pts',(-9.33302725419171,0.827511455077708,
15.));
#30116=CARTESIAN_POINT('Ctrl Pts',(-9.31662674801348,0.845709935759477,
15.));
#30117=CARTESIAN_POINT('Ctrl Pts',(-9.30887462895217,0.85431191349399,15.));
#30118=CARTESIAN_POINT('Ctrl Pts',(-9.30098899082769,0.862804079549591,
15.));
#30119=CARTESIAN_POINT('Ctrl Pts',(-9.29297263500711,0.87118408475251,15.));
#30120=CARTESIAN_POINT('Ctrl Pts',(-9.28554491584687,0.878948750718174,
15.));
#30121=CARTESIAN_POINT('Ctrl Pts',(-9.27801067856311,0.886611083762791,
15.));
#30122=CARTESIAN_POINT('Ctrl Pts',(-9.27037651112731,0.894165897788687,
15.));
#30123=CARTESIAN_POINT('Ctrl Pts',(-9.23471847327201,0.929453287905647,
15.));
#30124=CARTESIAN_POINT('Ctrl Pts',(-9.19685848483383,0.962423813168413,
15.));
#30125=CARTESIAN_POINT('Ctrl Pts',(-9.15706790102718,0.992921938496583,
15.));
#30126=CARTESIAN_POINT('Ctrl Pts',(-9.1348200881594,1.00997412824118,15.));
#30127=CARTESIAN_POINT('Ctrl Pts',(-9.11196791201093,1.02625290646587,15.));
#30128=CARTESIAN_POINT('Ctrl Pts',(-9.08855346078412,1.04172647599397,15.));
#30129=CARTESIAN_POINT('Ctrl Pts',(-9.07636608581335,1.0497805701151,15.));
#30130=CARTESIAN_POINT('Ctrl Pts',(-9.06402408681735,1.05761758254984,15.));
#30131=CARTESIAN_POINT('Ctrl Pts',(-9.05155350308553,1.06522083003624,15.));
#30132=CARTESIAN_POINT('Ctrl Pts',(-9.00599347684328,1.09299853174258,15.));
#30133=CARTESIAN_POINT('Ctrl Pts',(-8.95866634904485,1.11769704489194,15.));
#30134=CARTESIAN_POINT('Ctrl Pts',(-8.9098714082964,1.13911581419075,15.));
#30135=CARTESIAN_POINT('Ctrl Pts',(-8.87875621717539,1.15277397403451,15.));
#30136=CARTESIAN_POINT('Ctrl Pts',(-8.84704321113986,1.16509767556388,15.));
#30137=CARTESIAN_POINT('Ctrl Pts',(-8.81482207543407,1.17607856395778,15.));
#30138=CARTESIAN_POINT('Ctrl Pts',(-9.5500522825869,-1.91003407042144E-5,
14.0658930328476));
#30139=CARTESIAN_POINT('Ctrl Pts',(-9.55009297052377,-0.0583092030762354,
14.0685430772439));
#30140=CARTESIAN_POINT('Ctrl Pts',(-9.54531553472187,-0.116592705360584,
14.0711931216402));
#30141=CARTESIAN_POINT('Ctrl Pts',(-9.53565805831561,-0.174056052177473,
14.0738431660365));
#30142=CARTESIAN_POINT('Ctrl Pts',(-9.50753168118462,-0.34141196336918,
14.0815611396529));
#30143=CARTESIAN_POINT('Ctrl Pts',(-9.43801260792104,-0.501811283663713,
14.0892791132692));
#30144=CARTESIAN_POINT('Ctrl Pts',(-9.33511600940998,-0.636760844971574,
14.0969970868856));
#30145=CARTESIAN_POINT('Ctrl Pts',(-9.23221941089891,-0.771710406279434,
14.104715060502));
#30146=CARTESIAN_POINT('Ctrl Pts',(-9.09594528714036,-0.881210208600624,
14.1124330341183));
#30147=CARTESIAN_POINT('Ctrl Pts',(-8.94200530253875,-0.952635520799005,
14.1201510077347));
#30148=CARTESIAN_POINT('Ctrl Pts',(-8.78806531793715,-1.02406083299739,
14.127868981351));
#30149=CARTESIAN_POINT('Ctrl Pts',(-8.61645947249249,-1.05741165507296,
14.1355869549674));
#30150=CARTESIAN_POINT('Ctrl Pts',(-8.44697298591488,-1.04884281887132,
14.1433049285838));
#30151=CARTESIAN_POINT('Ctrl Pts',(-8.27748649933728,-1.04027398266968,
14.1510229022001));
#30152=CARTESIAN_POINT('Ctrl Pts',(-8.11011937162673,-0.989785488190817,
14.1587408758165));
#30153=CARTESIAN_POINT('Ctrl Pts',(-7.96416812134215,-0.903198383936824,
14.1664588494329));
#30154=CARTESIAN_POINT('Ctrl Pts',(-7.81821687105758,-0.816611279682832,
14.1741768230492));
#30155=CARTESIAN_POINT('Ctrl Pts',(-7.69368149819898,-0.693925565653706,
14.1818947966656));
#30156=CARTESIAN_POINT('Ctrl Pts',(-7.60492025322581,-0.549286236716252,
14.1896127702819));
#30157=CARTESIAN_POINT('Ctrl Pts',(-7.51615900825265,-0.404646907778796,
14.1973307438983));
#30158=CARTESIAN_POINT('Ctrl Pts',(-7.46317189116493,-0.238053963933011,
14.2050487175147));
#30159=CARTESIAN_POINT('Ctrl Pts',(-7.45206802806561,-0.0687146645719171,
14.212766691131));
#30160=CARTESIAN_POINT('Ctrl Pts',(-7.4409641649663,0.100624634789177,14.2204846647474));
#30161=CARTESIAN_POINT('Ctrl Pts',(-7.4717435558554,0.272710289665581,14.2282026383638));
#30162=CARTESIAN_POINT('Ctrl Pts',(-7.54085750454635,0.427701760980757,
14.2359206119801));
#30163=CARTESIAN_POINT('Ctrl Pts',(-7.6099714532373,0.582693232295935,14.2436385855965));
#30164=CARTESIAN_POINT('Ctrl Pts',(-7.7174199597301,0.720590520049885,14.2513565592128));
#30165=CARTESIAN_POINT('Ctrl Pts',(-7.85081479623634,0.825494817757516,
14.2590745328292));
#30166=CARTESIAN_POINT('Ctrl Pts',(-7.98420963274259,0.930399115465145,
14.2667925064456));
#30167=CARTESIAN_POINT('Ctrl Pts',(-8.14355079926228,1.00231042312646,14.2745104800619));
#30168=CARTESIAN_POINT('Ctrl Pts',(-8.31046712684085,1.03293775849401,14.2822284536783));
#30169=CARTESIAN_POINT('Ctrl Pts',(-8.47738345441942,1.06356509386157,14.2899464272947));
#30170=CARTESIAN_POINT('Ctrl Pts',(-8.65187494305688,1.05290845693537,14.297664400911));
#30171=CARTESIAN_POINT('Ctrl Pts',(-8.81382367414481,1.00219649993237,14.3053823745274));
#30172=CARTESIAN_POINT('Ctrl Pts',(-8.97577240523274,0.951484542929382,
14.3131003481437));
#30173=CARTESIAN_POINT('Ctrl Pts',(-9.12517837877114,0.860717265849599,
14.3208183217601));
#30174=CARTESIAN_POINT('Ctrl Pts',(-9.24481589946291,0.740359641551137,
14.3285362953765));
#30175=CARTESIAN_POINT('Ctrl Pts',(-9.36445342015469,0.620002017252674,
14.3362542689928));
#30176=CARTESIAN_POINT('Ctrl Pts',(-9.45432248799984,0.470054045735534,
14.3439722426092));
#30177=CARTESIAN_POINT('Ctrl Pts',(-9.5040616887745,0.307803911712927,14.3516902162256));
#30178=CARTESIAN_POINT('Ctrl Pts',(-9.53457214754885,0.208278266987425,
14.3564244884329));
#30179=CARTESIAN_POINT('Ctrl Pts',(-9.54998293159569,0.104123684619262,
14.3611587606403));
#30180=CARTESIAN_POINT('Ctrl Pts',(-9.55003832846065,-1.48519270705213E-5,
14.3658930328476));
#30181=CARTESIAN_POINT('Ctrl Pts',(-8.81478889550439,1.17604951161383,13.8));
#30182=CARTESIAN_POINT('Ctrl Pts',(-8.86280079884564,1.15963858656941,13.8));
#30183=CARTESIAN_POINT('Ctrl Pts',(-8.90960853485214,1.14022107018164,13.8));
#30184=CARTESIAN_POINT('Ctrl Pts',(-8.95497423007167,1.11798781340007,13.8));
#30185=CARTESIAN_POINT('Ctrl Pts',(-9.00031750369391,1.09576554521081,13.8));
#30186=CARTESIAN_POINT('Ctrl Pts',(-9.04422105970477,1.07072961904385,13.8));
#30187=CARTESIAN_POINT('Ctrl Pts',(-9.08642013951975,1.04302636820761,13.8));
#30188=CARTESIAN_POINT('Ctrl Pts',(-9.12519890659286,1.0175685166133,13.8));
#30189=CARTESIAN_POINT('Ctrl Pts',(-9.16253852722804,0.989857330873132,
13.8));
#30190=CARTESIAN_POINT('Ctrl Pts',(-9.1982035077309,0.959980834798695,13.8));
#30191=CARTESIAN_POINT('Ctrl Pts',(-9.20529926268142,0.954036732434542,
13.8));
#30192=CARTESIAN_POINT('Ctrl Pts',(-9.21233027103493,0.948005400253259,
13.8));
#30193=CARTESIAN_POINT('Ctrl Pts',(-9.21928917146909,0.941892145754135,
13.8));
#30194=CARTESIAN_POINT('Ctrl Pts',(-9.24730738764004,0.917278704638696,
13.8));
#30195=CARTESIAN_POINT('Ctrl Pts',(-9.27408805651624,0.891400484316834,
13.8));
#30196=CARTESIAN_POINT('Ctrl Pts',(-9.29952971553077,0.864321783055097,
13.8));
#30197=CARTESIAN_POINT('Ctrl Pts',(-9.33347410635491,0.828193242140612,
13.8));
#30198=CARTESIAN_POINT('Ctrl Pts',(-9.36503686827907,0.789928317341295,
13.8));
#30199=CARTESIAN_POINT('Ctrl Pts',(-9.394068236154,0.749793332929783,13.8));
#30200=CARTESIAN_POINT('Ctrl Pts',(-9.41426345293716,0.721874059050893,
13.8));
#30201=CARTESIAN_POINT('Ctrl Pts',(-9.43323285619316,0.693049121192648,
13.8));
#30202=CARTESIAN_POINT('Ctrl Pts',(-9.45091232284862,0.663402424323938,
13.8));
#30203=CARTESIAN_POINT('Ctrl Pts',(-9.4603430291963,0.647588073258055,13.8));
#30204=CARTESIAN_POINT('Ctrl Pts',(-9.46940649045895,0.631539836461061,
13.8));
#30205=CARTESIAN_POINT('Ctrl Pts',(-9.47809152424505,0.615270194622729,
13.8));
#30206=CARTESIAN_POINT('Ctrl Pts',(-9.48251143380655,0.606990394302504,
13.8));
#30207=CARTESIAN_POINT('Ctrl Pts',(-9.48683331758414,0.5986532504956,13.8));
#30208=CARTESIAN_POINT('Ctrl Pts',(-9.49105559547924,0.590260402670554,
13.8));
#30209=CARTESIAN_POINT('Ctrl Pts',(-9.49557755522519,0.581271861186176,
13.8));
#30210=CARTESIAN_POINT('Ctrl Pts',(-9.49998189717905,0.572225974771678,
13.8));
#30211=CARTESIAN_POINT('Ctrl Pts',(-9.50426389034573,0.563132325953286,
13.8));
#30212=CARTESIAN_POINT('Ctrl Pts',(-9.52493506409048,0.519233051157331,
13.8));
#30213=CARTESIAN_POINT('Ctrl Pts',(-9.54278546875511,0.474169441819486,
13.8));
#30214=CARTESIAN_POINT('Ctrl Pts',(-9.55766761541056,0.42818903643647,13.8));
#30215=CARTESIAN_POINT('Ctrl Pts',(-9.56297848681177,0.411780380775562,
13.8));
#30216=CARTESIAN_POINT('Ctrl Pts',(-9.56791089342669,0.395254820533891,
13.8));
#30217=CARTESIAN_POINT('Ctrl Pts',(-9.57245655696628,0.378623239143664,
13.8));
#30218=CARTESIAN_POINT('Ctrl Pts',(-9.58437734139714,0.335007715299727,
13.8));
#30219=CARTESIAN_POINT('Ctrl Pts',(-9.59364116996622,0.290662748326304,
13.8));
#30220=CARTESIAN_POINT('Ctrl Pts',(-9.60021783074656,0.245835590658758,
13.8));
#30221=CARTESIAN_POINT('Ctrl Pts',(-9.60298141730899,0.226998716643231,
13.8));
#30222=CARTESIAN_POINT('Ctrl Pts',(-9.60527003510969,0.208076747567834,
13.8));
#30223=CARTESIAN_POINT('Ctrl Pts',(-9.60707938280791,0.189088469737628,
13.8));
#30224=CARTESIAN_POINT('Ctrl Pts',(-9.60796926912187,0.179749519250995,
13.8));
#30225=CARTESIAN_POINT('Ctrl Pts',(-9.60874333971694,0.170392564265823,
13.8));
#30226=CARTESIAN_POINT('Ctrl Pts',(-9.60940054471547,0.161026142289271,
13.8));
#30227=CARTESIAN_POINT('Ctrl Pts',(-9.61273653439172,0.113481940576065,
13.8));
#30228=CARTESIAN_POINT('Ctrl Pts',(-9.61305375823859,0.065881512589885,
13.8));
#30229=CARTESIAN_POINT('Ctrl Pts',(-9.6103548789984,0.0185137348807834,
13.8));
#30230=CARTESIAN_POINT('Ctrl Pts',(-9.60768657879641,-0.0283173529821776,
13.8));
#30231=CARTESIAN_POINT('Ctrl Pts',(-9.60206995434507,-0.0749221057539117,
13.8));
#30232=CARTESIAN_POINT('Ctrl Pts',(-9.59345810572669,-0.121012288686138,
13.8));
#30233=CARTESIAN_POINT('Ctrl Pts',(-9.59107622215987,-0.133760010363862,
13.8));
#30234=CARTESIAN_POINT('Ctrl Pts',(-9.5884649252658,-0.146468262729219,
13.8));
#30235=CARTESIAN_POINT('Ctrl Pts',(-9.58562257062166,-0.159130656277011,
13.8));
#30236=CARTESIAN_POINT('Ctrl Pts',(-9.580683856266,-0.181132113737854,13.8));
#30237=CARTESIAN_POINT('Ctrl Pts',(-9.57504766985512,-0.202995218741589,
13.8));
#30238=CARTESIAN_POINT('Ctrl Pts',(-9.56872395555178,-0.224688164794557,
13.8));
#30239=CARTESIAN_POINT('Ctrl Pts',(-9.56551399339403,-0.235699657815915,
13.8));
#30240=CARTESIAN_POINT('Ctrl Pts',(-9.56212684590213,-0.246667280396052,
13.8));
#30241=CARTESIAN_POINT('Ctrl Pts',(-9.55856361622354,-0.257586691768621,
13.8));
#30242=CARTESIAN_POINT('Ctrl Pts',(-9.55533502617401,-0.267480609950803,
13.8));
#30243=CARTESIAN_POINT('Ctrl Pts',(-9.55196447513525,-0.27732683973438,
13.8));
#30244=CARTESIAN_POINT('Ctrl Pts',(-9.54845493647163,-0.287118339294702,
13.8));
#30245=CARTESIAN_POINT('Ctrl Pts',(-9.53268023941429,-0.331129234772824,
13.8));
#30246=CARTESIAN_POINT('Ctrl Pts',(-9.51409214385052,-0.374063802247248,
13.8));
#30247=CARTESIAN_POINT('Ctrl Pts',(-9.49280934665199,-0.415647420881541,
13.8));
#30248=CARTESIAN_POINT('Ctrl Pts',(-9.48095698558012,-0.438805282046661,
13.8));
#30249=CARTESIAN_POINT('Ctrl Pts',(-9.4682681093108,-0.461543689934097,
13.8));
#30250=CARTESIAN_POINT('Ctrl Pts',(-9.4547579204182,-0.483810537438775,
13.8));
#30251=CARTESIAN_POINT('Ctrl Pts',(-9.44902419320865,-0.49326059253597,
13.8));
#30252=CARTESIAN_POINT('Ctrl Pts',(-9.4431430707807,-0.502624468776889,
13.8));
#30253=CARTESIAN_POINT('Ctrl Pts',(-9.43712256581291,-0.51188805590247,
13.8));
#30254=CARTESIAN_POINT('Ctrl Pts',(-9.41182946395985,-0.550805863286665,
13.8));
#30255=CARTESIAN_POINT('Ctrl Pts',(-9.38404926471349,-0.588007002160364,
13.8));
#30256=CARTESIAN_POINT('Ctrl Pts',(-9.35388332257603,-0.623204245519968,
13.8));
#30257=CARTESIAN_POINT('Ctrl Pts',(-9.33467669468324,-0.645614298319899,
13.8));
#30258=CARTESIAN_POINT('Ctrl Pts',(-9.31450202461069,-0.667211228483348,
13.8));
#30259=CARTESIAN_POINT('Ctrl Pts',(-9.29341905289388,-0.68794083902027,
13.8));
#30260=CARTESIAN_POINT('Origin',(-8.5,0.,15.));
#30261=CARTESIAN_POINT('',(-7.46076951545867,-1.8,15.));
#30262=CARTESIAN_POINT('',(-6.42153903091735,0.,15.));
#30263=CARTESIAN_POINT('',(-7.46076951545867,-1.8,15.));
#30264=CARTESIAN_POINT('',(-7.46076951545867,1.8,15.));
#30265=CARTESIAN_POINT('',(-6.42153903091735,0.,15.));
#30266=CARTESIAN_POINT('',(-9.53923048454133,1.8,15.));
#30267=CARTESIAN_POINT('',(-7.46076951545867,1.8,15.));
#30268=CARTESIAN_POINT('',(-10.5784609690827,2.22044604925031E-16,15.));
#30269=CARTESIAN_POINT('',(-9.53923048454133,1.8,15.));
#30270=CARTESIAN_POINT('',(-9.53923048454133,-1.8,15.));
#30271=CARTESIAN_POINT('',(-10.5784609690827,2.54538057293978E-16,15.));
#30272=CARTESIAN_POINT('',(-9.53923048454133,-1.8,15.));
#30273=CARTESIAN_POINT('Origin',(-8.5,0.,13.7));
#30274=CARTESIAN_POINT('Origin',(-9.53923048454133,-1.8,13.8));
#30275=CARTESIAN_POINT('',(-9.53923048454133,-1.8,13.8));
#30276=CARTESIAN_POINT('',(-7.46076951545867,-1.8,13.8));
#30277=CARTESIAN_POINT('',(-9.53923048454133,-1.8,13.8));
#30278=CARTESIAN_POINT('',(-7.46076951545867,-1.8,13.8));
#30279=CARTESIAN_POINT('',(-9.53923048454133,-1.8,13.8));
#30280=CARTESIAN_POINT('Origin',(-10.5784609690827,2.54538057293978E-16,
13.8));
#30281=CARTESIAN_POINT('',(-10.5784609690827,2.54538057293978E-16,13.8));
#30282=CARTESIAN_POINT('',(-10.5784609690827,2.54538057293978E-16,13.8));
#30283=CARTESIAN_POINT('',(-10.5784609690827,2.54538057293978E-16,13.8));
#30284=CARTESIAN_POINT('Origin',(-9.53923048454133,1.8,13.8));
#30285=CARTESIAN_POINT('',(-9.53923048454133,1.8,13.8));
#30286=CARTESIAN_POINT('',(-9.53923048454133,1.8,13.8));
#30287=CARTESIAN_POINT('',(-9.53923048454133,1.8,13.8));
#30288=CARTESIAN_POINT('Origin',(-7.46076951545867,1.8,13.8));
#30289=CARTESIAN_POINT('',(-7.46076951545867,1.8,13.8));
#30290=CARTESIAN_POINT('',(-7.46076951545867,1.8,13.8));
#30291=CARTESIAN_POINT('',(-7.46076951545867,1.8,13.8));
#30292=CARTESIAN_POINT('Origin',(-6.42153903091735,0.,13.8));
#30293=CARTESIAN_POINT('',(-6.42153903091735,0.,13.8));
#30294=CARTESIAN_POINT('',(-6.42153903091735,0.,13.8));
#30295=CARTESIAN_POINT('',(-6.42153903091735,0.,13.8));
#30296=CARTESIAN_POINT('Origin',(-7.46076951545867,-1.8,13.8));
#30297=CARTESIAN_POINT('',(-7.46076951545867,-1.8,13.8));
#30298=CARTESIAN_POINT('Origin',(-8.5,0.,13.8));
#34397=UNCERTAINTY_MEASURE_WITH_UNIT(LENGTH_MEASURE(0.001),#34434,
'DISTANCE_ACCURACY_VALUE',
'Maximum model space distance between geometric entities at asserted c
onnectivities');
#34404=UNCERTAINTY_MEASURE_WITH_UNIT(LENGTH_MEASURE(0.001),#34434,
'DISTANCE_ACCURACY_VALUE',
'Maximum model space distance between geometric entities at asserted c
onnectivities');
#34426=(
GEOMETRIC_REPRESENTATION_CONTEXT(3)
GLOBAL_UNCERTAINTY_ASSIGNED_CONTEXT((#34397))
GLOBAL_UNIT_ASSIGNED_CONTEXT((#34434,#34436,#34437))
REPRESENTATION_CONTEXT('','3D')
);
#34433=(
GEOMETRIC_REPRESENTATION_CONTEXT(3)
GLOBAL_UNCERTAINTY_ASSIGNED_CONTEXT((#34404))
GLOBAL_UNIT_ASSIGNED_CONTEXT((#34434,#34436,#34437))
REPRESENTATION_CONTEXT('','3D')
);
#34434=(
LENGTH_UNIT()
NAMED_UNIT(*)
SI_UNIT(.CENTI.,.METRE.)
);
#34436=(
NAMED_UNIT(*)
PLANE_ANGLE_UNIT()
SI_UNIT($,.RADIAN.)
);
#34437=(
NAMED_UNIT(*)
SI_UNIT($,.STERADIAN.)
SOLID_ANGLE_UNIT()
);
#34459=SHAPE_DEFINITION_REPRESENTATION(#34521,#34558);
#34521=PRODUCT_DEFINITION_SHAPE('',$,#34587);
#34558=SHAPE_REPRESENTATION('',(#9621),#34426);
#34565=PRODUCT_DEFINITION_CONTEXT('part definition',#34651,'design');
#34587=PRODUCT_DEFINITION('M24 adjustment nut','M24 adjustment nut',#34615,
#34565);
#34615=PRODUCT_DEFINITION_FORMATION('',$,#34674);
#34651=APPLICATION_CONTEXT(
'Core Data for Automotive Mechanical Design Process');
#34652=PRODUCT_CONTEXT('part definition',#34651,'mechanical');
#34674=PRODUCT('M24 adjustment nut','M24 adjustment nut',
'M24 adjustment nut',(#34652));
#34744=COLOUR_RGB('Black',0.12,0.14,0.17);
#34745=FILL_AREA_STYLE_COLOUR('',#34744);
#34746=FILL_AREA_STYLE('',(#34745));
#34747=SURFACE_STYLE_FILL_AREA(#34746);
#34748=SURFACE_SIDE_STYLE('',(#34747));
#34749=SURFACE_STYLE_USAGE(.BOTH.,#34748);
#34750=PRESENTATION_STYLE_ASSIGNMENT((#34749));
ENDSEC;
END-ISO-10303-21;
